ISO-10303-21;
HEADER;
FILE_DESCRIPTION (('STEP AP214'),
    '1' );
FILE_NAME ('Part11^Assem2.step',
    '2026-11-01T06:29:40',
    ( '' ),
    ( '' ),
    'SwSTEP 2.0',
    'SolidWorks 2024',
    '' );
FILE_SCHEMA (( 'AUTOMOTIVE_DESIGN' ));
ENDSEC;

DATA;
#7=DIRECTION ( 'NONE',  ( -0.000000000000000000, -0.000000000000000000, 1.000000000000000000 ) ) ;
#10=EDGE_CURVE ( 'NONE', #8032, #20154, #10638, .T. ) ;
#13=CARTESIAN_POINT ( 'NONE',  ( 498.8334540492693918, 191.8198460455371333, 24.99421986894476078 ) ) ;
#38=ORIENTED_EDGE ( 'NONE', *, *, #17930, .F. ) ;
#43=FACE_OUTER_BOUND ( 'NONE', #9378, .T. ) ;
#54=PLANE ( 'NONE',  #1356 ) ;
#67=ORIENTED_EDGE ( 'NONE', *, *, #2522, .F. ) ;
#69=FILL_AREA_STYLE_COLOUR ( '', #11687 ) ;
#84=AXIS2_PLACEMENT_3D ( 'NONE', #6043, #6351, #15948 ) ;
#89=VECTOR ( 'NONE', #7, 1000.000000000000000 ) ;
#98=DIRECTION ( 'NONE',  ( 0.000000000000000000, 0.000000000000000000, -1.000000000000000000 ) ) ;
#104=SURFACE_STYLE_USAGE ( .BOTH. , #15704 ) ;
#110=COLOUR_RGB ( '', 0.40784314, 0.44705882, 0.49803922) ;
#124=CARTESIAN_POINT ( 'NONE',  ( 463.8334540492693350, 214.2156642432025251, 250.0000000000000000 ) ) ;
#128=ORIENTED_EDGE ( 'NONE', *, *, #4695, .T. ) ;
#136=ORIENTED_EDGE ( 'NONE', *, *, #16204, .F. ) ;
#145=CIRCLE ( 'NONE', #2460, 10.00000000000000888 ) ;
#148=DIRECTION ( 'NONE',  ( 1.000000000000000000, -0.000000000000000000, -0.000000000000000000 ) ) ;
#156=FILL_AREA_STYLE_COLOUR ( '', #13786 ) ;
#165=PRESENTATION_STYLE_ASSIGNMENT (( #8000 ) ) ;
#167=CIRCLE ( 'NONE', #19893, 10.00000000000001066 ) ;
#176=SURFACE_STYLE_FILL_AREA ( #14295 ) ;
#186=VECTOR ( 'NONE', #8676, 1000.000000000000000 ) ;
#219=ADVANCED_FACE ( 'NONE', ( #3459 ), #14966, .T. ) ;
#239=ADVANCED_FACE ( 'NONE', ( #10427 ), #20293, .T. ) ;
#246=SURFACE_SIDE_STYLE ('',( #6343 ) ) ;
#266=( LENGTH_UNIT ( ) NAMED_UNIT ( * ) SI_UNIT ( .MILLI., .METRE. ) );
#268=VECTOR ( 'NONE', #14783, 1000.000000000000000 ) ;
#273=EDGE_LOOP ( 'NONE', ( #888, #7387 ) ) ;
#290=CIRCLE ( 'NONE', #19687, 10.00000000000001066 ) ;
#293=COLOUR_RGB ( '', 0.31764706, 0.68627451, 0.89019608) ;
#327=SURFACE_SIDE_STYLE ('',( #8181 ) ) ;
#334=CARTESIAN_POINT ( 'NONE',  ( 486.8117674897343363, 134.2156642432025251, 245.0000000000000000 ) ) ;
#346=FACE_OUTER_BOUND ( 'NONE', #5460, .T. ) ;
#355=( NAMED_UNIT ( * ) SI_UNIT ( $, .STERADIAN. ) SOLID_ANGLE_UNIT ( ) );
#384=ORIENTED_EDGE ( 'NONE', *, *, #13185, .T. ) ;
#385=EDGE_CURVE ( 'NONE', #13659, #12399, #1618, .T. ) ;
#387=COLOUR_RGB ( '', 0.72549020, 0.75294118, 0.79215686) ;
#391=EDGE_LOOP ( 'NONE', ( #10090, #136, #7141, #4283 ) ) ;
#393=DIRECTION ( 'NONE',  ( -1.000000000000000000, 0.000000000000000000, 0.000000000000000000 ) ) ;
#417=VERTEX_POINT ( 'NONE', #9571 ) ;
#423=UNCERTAINTY_MEASURE_WITH_UNIT (LENGTH_MEASURE( 1.000000000000000082E-05 ), #18425, 'distance_accuracy_value', 'NONE');
#432=AXIS2_PLACEMENT_3D ( 'NONE', #1849, #20297, #3101 ) ;
#434=FACE_OUTER_BOUND ( 'NONE', #2363, .T. ) ;
#460=CARTESIAN_POINT ( 'NONE',  ( 486.8117674897343363, 214.2156642432025251, 250.0000000000000000 ) ) ;
#476=EDGE_CURVE ( 'NONE', #17048, #8243, #2236, .T. ) ;
#479=FILL_AREA_STYLE_COLOUR ( '', #3345 ) ;
#492=DIRECTION ( 'NONE',  ( 0.000000000000000000, 0.000000000000000000, 1.000000000000000000 ) ) ;
#511=CARTESIAN_POINT ( 'NONE',  ( 463.8334540492693350, 191.8198460455371333, 235.0057801310552463 ) ) ;
#519=PRESENTATION_STYLE_ASSIGNMENT (( #5068 ) ) ;
#534=LINE ( 'NONE', #11248, #9722 ) ;
#544=ORIENTED_EDGE ( 'NONE', *, *, #15177, .T. ) ;
#563=SURFACE_STYLE_FILL_AREA ( #8590 ) ;
#564=CARTESIAN_POINT ( 'NONE',  ( 475.8334540492694487, 214.2156642432025251, 250.0000000000000000 ) ) ;
#579=CARTESIAN_POINT ( 'NONE',  ( 458.8334540492693350, 191.8198460455371333, 91.76606011801541740 ) ) ;
#581=ORIENTED_EDGE ( 'NONE', *, *, #2414, .F. ) ;
#594=CARTESIAN_POINT ( 'NONE',  ( 463.8334540492693350, 214.2156642432025251, -87.31255586191144857 ) ) ;
#604=FACE_OUTER_BOUND ( 'NONE', #19997, .T. ) ;
#611=FACE_OUTER_BOUND ( 'NONE', #3674, .T. ) ;
#616=UNCERTAINTY_MEASURE_WITH_UNIT (LENGTH_MEASURE( 1.000000000000000082E-05 ), #11139, 'distance_accuracy_value', 'NONE');
#621=UNCERTAINTY_MEASURE_WITH_UNIT (LENGTH_MEASURE( 1.000000000000000082E-05 ), #1117, 'distance_accuracy_value', 'NONE');
#633=FILL_AREA_STYLE_COLOUR ( '', #9221 ) ;
#646=CARTESIAN_POINT ( 'NONE',  ( 463.8334540492693350, 191.8198460455371333, 24.99421986894476078 ) ) ;
#664=VERTEX_POINT ( 'NONE', #4311 ) ;
#672=EDGE_CURVE ( 'NONE', #5981, #6883, #1099, .T. ) ;
#676=ORIENTED_EDGE ( 'NONE', *, *, #12915, .T. ) ;
#691=EDGE_CURVE ( 'NONE', #17286, #13581, #15353, .T. ) ;
#700=AXIS2_PLACEMENT_3D ( 'NONE', #2118, #9651, #2004 ) ;
#701=CARTESIAN_POINT ( 'NONE',  ( 423.8334540492694487, 191.8198460455371333, 225.0057801310552463 ) ) ;
#714=FACE_OUTER_BOUND ( 'NONE', #5598, .T. ) ;
#716=VERTEX_POINT ( 'NONE', #12767 ) ;
#717=FILL_AREA_STYLE ('',( #10208 ) ) ;
#730=EDGE_LOOP ( 'NONE', ( #10944, #17357 ) ) ;
#734=COLOUR_RGB ( '', 0.66274510, 0.83137255, 0.94901961) ;
#746=PLANE ( 'NONE',  #16845 ) ;
#750=CARTESIAN_POINT ( 'NONE',  ( 463.8334540492693350, 214.2156642432025251, 250.0000000000000000 ) ) ;
#760=DIRECTION ( 'NONE',  ( 1.000000000000000000, 0.000000000000000000, 0.000000000000000000 ) ) ;
#770=LINE ( 'NONE', #11506, #19618 ) ;
#773=VECTOR ( 'NONE', #17341, 1000.000000000000000 ) ;
#804=( NAMED_UNIT ( * ) PLANE_ANGLE_UNIT ( ) SI_UNIT ( $, .RADIAN. ) );
#806=CARTESIAN_POINT ( 'NONE',  ( 423.8334540492694487, 191.8198460455371333, 225.0057801310552463 ) ) ;
#815=PRESENTATION_STYLE_ASSIGNMENT (( #13601 ) ) ;
#822=( GEOMETRIC_REPRESENTATION_CONTEXT ( 3 ) GLOBAL_UNCERTAINTY_ASSIGNED_CONTEXT ( ( #8467 ) ) GLOBAL_UNIT_ASSIGNED_CONTEXT ( ( #15028, #2641, #15338 ) ) REPRESENTATION_CONTEXT ( 'NONE', 'WORKASPACE' ) );
#827=ADVANCED_FACE ( 'NONE', ( #3490 ), #1593, .F. ) ;
#828=FILL_AREA_STYLE ('',( #10423 ) ) ;
#838=CARTESIAN_POINT ( 'NONE',  ( 498.8334540492693918, 191.8198460455371333, 71.76606011801538898 ) ) ;
#843=EDGE_CURVE ( 'NONE', #18080, #16176, #8398, .T. ) ;
#857=CYLINDRICAL_SURFACE ( 'NONE', #9362, 10.00000000000000888 ) ;
#880=CARTESIAN_POINT ( 'NONE',  ( 503.8334540492693918, 0.000000000000000000, 250.0000000000000000 ) ) ;
#884=PLANE ( 'NONE',  #5653 ) ;
#886=VERTEX_POINT ( 'NONE', #9864 ) ;
#888=ORIENTED_EDGE ( 'NONE', *, *, #3213, .T. ) ;
#919=SURFACE_STYLE_USAGE ( .BOTH. , #15072 ) ;
#922=LINE ( 'NONE', #11883, #18596 ) ;
#925=ORIENTED_EDGE ( 'NONE', *, *, #1375, .F. ) ;
#939=PRESENTATION_STYLE_ASSIGNMENT (( #3960 ) ) ;
#951=VERTEX_POINT ( 'NONE', #4384 ) ;
#961=DIRECTION ( 'NONE',  ( -0.000000000000000000, 0.000000000000000000, 1.000000000000000000 ) ) ;
#977=ORIENTED_EDGE ( 'NONE', *, *, #9541, .F. ) ;
#984=LINE ( 'NONE', #7121, #16144 ) ;
#986=DIRECTION ( 'NONE',  ( 1.000000000000000000, 0.000000000000000000, -0.000000000000000000 ) ) ;
#994=AXIS2_PLACEMENT_3D ( 'NONE', #4735, #17489, #9561 ) ;
#1008=CARTESIAN_POINT ( 'NONE',  ( 503.8334540492693918, 191.8198460455371333, 168.2339398819845826 ) ) ;
#1009=ADVANCED_FACE ( 'NONE', ( #12037 ), #19722, .F. ) ;
#1012=FACE_OUTER_BOUND ( 'NONE', #5998, .T. ) ;
#1044=EDGE_CURVE ( 'NONE', #8848, #15257, #17264, .T. ) ;
#1050=EDGE_LOOP ( 'NONE', ( #9283, #18605, #18506, #2187 ) ) ;
#1065=DIRECTION ( 'NONE',  ( -0.000000000000000000, -0.000000000000000000, 1.000000000000000000 ) ) ;
#1075=VECTOR ( 'NONE', #13463, 1000.000000000000000 ) ;
#1083=AXIS2_PLACEMENT_3D ( 'NONE', #646, #16252, #11584 ) ;
#1089=FACE_BOUND ( 'NONE', #14856, .T. ) ;
#1095=( LENGTH_UNIT ( ) NAMED_UNIT ( * ) SI_UNIT ( .MILLI., .METRE. ) );
#1096=SURFACE_STYLE_USAGE ( .BOTH. , #10502 ) ;
#1099=CIRCLE ( 'NONE', #14624, 10.00000000000000888 ) ;
#1109=CARTESIAN_POINT ( 'NONE',  ( 498.8334540492693918, 191.8198460455371333, 81.76606011801540319 ) ) ;
#1113=DIRECTION ( 'NONE',  ( 1.000000000000000000, 0.000000000000000000, 0.000000000000000000 ) ) ;
#1115=CARTESIAN_POINT ( 'NONE',  ( 423.8334540492694487, 191.8198460455371333, 24.99421986894476078 ) ) ;
#1117=( LENGTH_UNIT ( ) NAMED_UNIT ( * ) SI_UNIT ( .MILLI., .METRE. ) );
#1120=DIRECTION ( 'NONE',  ( 0.000000000000000000, 0.000000000000000000, -1.000000000000000000 ) ) ;
#1127=COLOUR_RGB ( '', 0.31764706, 0.68627451, 0.89019608) ;
#1139=STYLED_ITEM ( 'NONE', ( #5982 ), #9261 ) ;
#1150=COLOUR_RGB ( '', 0.31764706, 0.68627451, 0.89019608) ;
#1151=ADVANCED_FACE ( 'NONE', ( #9220 ), #14267, .F. ) ;
#1182=ORIENTED_EDGE ( 'NONE', *, *, #10165, .F. ) ;
#1194=( NAMED_UNIT ( * ) PLANE_ANGLE_UNIT ( ) SI_UNIT ( $, .RADIAN. ) );
#1202=ORIENTED_EDGE ( 'NONE', *, *, #15177, .F. ) ;
#1214=( NAMED_UNIT ( * ) SI_UNIT ( $, .STERADIAN. ) SOLID_ANGLE_UNIT ( ) );
#1222=ORIENTED_EDGE ( 'NONE', *, *, #14307, .F. ) ;
#1236=FILL_AREA_STYLE_COLOUR ( '', #12312 ) ;
#1249=EDGE_CURVE ( 'NONE', #13405, #11940, #5119, .T. ) ;
#1258=EDGE_CURVE ( 'NONE', #13299, #7205, #13069, .T. ) ;
#1266=DIRECTION ( 'NONE',  ( -0.000000000000000000, 0.000000000000000000, 1.000000000000000000 ) ) ;
#1276=CARTESIAN_POINT ( 'NONE',  ( 475.8334540492694487, 214.2156642432025251, 245.0000000000000000 ) ) ;
#1278=PRESENTATION_STYLE_ASSIGNMENT (( #16794 ) ) ;
#1279=VERTEX_POINT ( 'NONE', #5822 ) ;
#1280=PRESENTATION_STYLE_ASSIGNMENT (( #9062 ) ) ;
#1292=FILL_AREA_STYLE ('',( #15463 ) ) ;
#1304=( NAMED_UNIT ( * ) SI_UNIT ( $, .STERADIAN. ) SOLID_ANGLE_UNIT ( ) );
#1311=SURFACE_STYLE_FILL_AREA ( #9695 ) ;
#1312=LINE ( 'NONE', #2991, #18186 ) ;
#1325=CARTESIAN_POINT ( 'NONE',  ( 423.8334540492694487, 191.8198460455371333, 215.0057801310552179 ) ) ;
#1326=FACE_OUTER_BOUND ( 'NONE', #10310, .T. ) ;
#1330=CARTESIAN_POINT ( 'NONE',  ( 463.8334540492693350, 134.2156642432025251, 0.000000000000000000 ) ) ;
#1352=DIRECTION ( 'NONE',  ( 1.000000000000000000, -0.000000000000000000, -0.000000000000000000 ) ) ;
#1356=AXIS2_PLACEMENT_3D ( 'NONE', #4603, #3257, #9534 ) ;
#1361=LINE ( 'NONE', #4600, #18892 ) ;
#1363=CARTESIAN_POINT ( 'NONE',  ( 423.8334540492694487, 191.8198460455371333, 71.76606011801538898 ) ) ;
#1375=EDGE_CURVE ( 'NONE', #11798, #16010, #10956, .T. ) ;
#1379=ORIENTED_EDGE ( 'NONE', *, *, #13450, .F. ) ;
#1381=ORIENTED_EDGE ( 'NONE', *, *, #7588, .T. ) ;
#1390=EDGE_CURVE ( 'NONE', #6575, #6561, #3224, .T. ) ;
#1391=FILL_AREA_STYLE_COLOUR ( '', #8532 ) ;
#1397=( GEOMETRIC_REPRESENTATION_CONTEXT ( 3 ) GLOBAL_UNCERTAINTY_ASSIGNED_CONTEXT ( ( #16729 ) ) GLOBAL_UNIT_ASSIGNED_CONTEXT ( ( #16168, #13080, #8314 ) ) REPRESENTATION_CONTEXT ( 'NONE', 'WORKASPACE' ) );
#1401=( NAMED_UNIT ( * ) PLANE_ANGLE_UNIT ( ) SI_UNIT ( $, .RADIAN. ) );
#1407=STYLED_ITEM ( 'NONE', ( #14471 ), #219 ) ;
#1422=FILL_AREA_STYLE ('',( #13724 ) ) ;
#1434=VECTOR ( 'NONE', #16449, 1000.000000000000000 ) ;
#1440=( GEOMETRIC_REPRESENTATION_CONTEXT ( 3 ) GLOBAL_UNCERTAINTY_ASSIGNED_CONTEXT ( ( #7259 ) ) GLOBAL_UNIT_ASSIGNED_CONTEXT ( ( #6985, #6799, #17791 ) ) REPRESENTATION_CONTEXT ( 'NONE', 'WORKASPACE' ) );
#1457=DIRECTION ( 'NONE',  ( 1.000000000000000000, 0.000000000000000000, 0.000000000000000000 ) ) ;
#1463=( NAMED_UNIT ( * ) SI_UNIT ( $, .STERADIAN. ) SOLID_ANGLE_UNIT ( ) );
#1471=ORIENTED_EDGE ( 'NONE', *, *, #1375, .T. ) ;
#1475=FILL_AREA_STYLE_COLOUR ( '', #12977 ) ;
#1480=SURFACE_SIDE_STYLE ('',( #7889 ) ) ;
#1487=( NAMED_UNIT ( * ) PLANE_ANGLE_UNIT ( ) SI_UNIT ( $, .RADIAN. ) );
#1492=ADVANCED_BREP_SHAPE_REPRESENTATION ( '', ( #15383, #15873, #2741 ), #19153 ) ;
#1512=( LENGTH_UNIT ( ) NAMED_UNIT ( * ) SI_UNIT ( .MILLI., .METRE. ) );
#1529=VECTOR ( 'NONE', #19046, 1000.000000000000000 ) ;
#1532=( NAMED_UNIT ( * ) PLANE_ANGLE_UNIT ( ) SI_UNIT ( $, .RADIAN. ) );
#1548=DIRECTION ( 'NONE',  ( 0.000000000000000000, 0.000000000000000000, 1.000000000000000000 ) ) ;
#1566=PLANE ( 'NONE',  #18276 ) ;
#1581=DIRECTION ( 'NONE',  ( -0.000000000000000000, 0.000000000000000000, -1.000000000000000000 ) ) ;
#1585=MECHANICAL_DESIGN_GEOMETRIC_PRESENTATION_REPRESENTATION('',(#3609),#3919);
#1592=AXIS2_PLACEMENT_3D ( 'NONE', #806, #4129, #13412 ) ;
#1593=CYLINDRICAL_SURFACE ( 'NONE', #11022, 10.00000000000000888 ) ;
#1598=CARTESIAN_POINT ( 'NONE',  ( 503.8334540492693918, 0.000000000000000000, 0.000000000000000000 ) ) ;
#1602=SURFACE_STYLE_FILL_AREA ( #2962 ) ;
#1614=ORIENTED_EDGE ( 'NONE', *, *, #9237, .F. ) ;
#1618=LINE ( 'NONE', #17626, #14274 ) ;
#1626=CARTESIAN_POINT ( 'NONE',  ( 406.3334540492693350, 242.8734308960556234, 250.0000000000000000 ) ) ;
#1636=ORIENTED_EDGE ( 'NONE', *, *, #12967, .F. ) ;
#1657=SURFACE_SIDE_STYLE ('',( #13848 ) ) ;
#1661=DIRECTION ( 'NONE',  ( 0.000000000000000000, 1.000000000000000000, 0.000000000000000000 ) ) ;
#1666=COLOUR_RGB ( '', 0.72549020, 0.75294118, 0.79215686) ;
#1673=SURFACE_STYLE_USAGE ( .BOTH. , #18901 ) ;
#1677=EDGE_CURVE ( 'NONE', #13170, #17444, #12472, .T. ) ;
#1688=FILL_AREA_STYLE ('',( #3165 ) ) ;
#1697=FILL_AREA_STYLE ('',( #18811 ) ) ;
#1713=EDGE_CURVE ( 'NONE', #8072, #4150, #8245, .T. ) ;
#1721=COLOUR_RGB ( '', 0.09019608, 0.27058824, 0.51372549) ;
#1722=AXIS2_PLACEMENT_3D ( 'NONE', #6869, #13154, #16754 ) ;
#1725=UNCERTAINTY_MEASURE_WITH_UNIT (LENGTH_MEASURE( 1.000000000000000082E-05 ), #15859, 'distance_accuracy_value', 'NONE');
#1737=EDGE_CURVE ( 'NONE', #13831, #12278, #8150, .T. ) ;
#1749=VECTOR ( 'NONE', #2238, 1000.000000000000000 ) ;
#1778=ORIENTED_EDGE ( 'NONE', *, *, #10679, .F. ) ;
#1794=CARTESIAN_POINT ( 'NONE',  ( 498.8334540492693918, 167.8734308960555950, 250.0000000000000000 ) ) ;
#1797=EDGE_CURVE ( 'NONE', #17228, #417, #17521, .T. ) ;
#1810=PRESENTATION_STYLE_ASSIGNMENT (( #16070 ) ) ;
#1816=ORIENTED_EDGE ( 'NONE', *, *, #4640, .T. ) ;
#1832=FILL_AREA_STYLE ('',( #17397 ) ) ;
#1833=EDGE_LOOP ( 'NONE', ( #12096, #18835 ) ) ;
#1837=VERTEX_POINT ( 'NONE', #14747 ) ;
#1842=DIRECTION ( 'NONE',  ( 1.000000000000000000, 1.197852309262419498E-15, -0.000000000000000000 ) ) ;
#1849=CARTESIAN_POINT ( 'NONE',  ( 498.8117674897343932, 191.8198460455371333, 81.76606011801540319 ) ) ;
#1860=CARTESIAN_POINT ( 'NONE',  ( 423.8334540492694487, 191.8198460455371333, 24.99421986894476078 ) ) ;
#1865=CARTESIAN_POINT ( 'NONE',  ( 458.8334540492693350, 191.8198460455371333, 178.2339398819846110 ) ) ;
#1875=ORIENTED_EDGE ( 'NONE', *, *, #9541, .T. ) ;
#1881=VECTOR ( 'NONE', #8183, 1000.000000000000000 ) ;
#1891=DIRECTION ( 'NONE',  ( -0.000000000000000000, 1.000000000000000000, -0.000000000000000000 ) ) ;
#1897=DIRECTION ( 'NONE',  ( 1.000000000000000000, -0.000000000000000000, -0.000000000000000000 ) ) ;
#1898=ORIENTED_EDGE ( 'NONE', *, *, #1713, .T. ) ;
#1903=FACE_OUTER_BOUND ( 'NONE', #10130, .T. ) ;
#1908=DIRECTION ( 'NONE',  ( 0.000000000000000000, 0.000000000000000000, 1.000000000000000000 ) ) ;
#1927=COLOUR_RGB ( '', 0.08235294, 0.09019608, 0.10196078) ;
#1931=CARTESIAN_POINT ( 'NONE',  ( 468.8334540492694487, 214.2156642432025251, 245.0000000000000000 ) ) ;
#1933=PRESENTATION_STYLE_ASSIGNMENT (( #16107 ) ) ;
#1943=( NAMED_UNIT ( * ) SI_UNIT ( $, .STERADIAN. ) SOLID_ANGLE_UNIT ( ) );
#1946=EDGE_CURVE ( 'NONE', #3481, #8072, #12029, .T. ) ;
#1947=LINE ( 'NONE', #11653, #16625 ) ;
#1960=ADVANCED_FACE ( 'NONE', ( #5672, #4240, #5481, #19664, #714 ), #2481, .T. ) ;
#1973=DIRECTION ( 'NONE',  ( -0.000000000000000000, -0.000000000000000000, 1.000000000000000000 ) ) ;
#1988=( NAMED_UNIT ( * ) SI_UNIT ( $, .STERADIAN. ) SOLID_ANGLE_UNIT ( ) );
#1994=PRESENTATION_STYLE_ASSIGNMENT (( #11595 ) ) ;
#1995=PRESENTATION_STYLE_ASSIGNMENT (( #11496 ) ) ;
#2004=DIRECTION ( 'NONE',  ( 0.000000000000000000, 0.000000000000000000, -1.000000000000000000 ) ) ;
#2015=DIRECTION ( 'NONE',  ( 0.000000000000000000, 0.000000000000000000, 1.000000000000000000 ) ) ;
#2019=DIRECTION ( 'NONE',  ( 1.000000000000000000, -0.000000000000000000, -0.000000000000000000 ) ) ;
#2029=CARTESIAN_POINT ( 'NONE',  ( 463.8334540492693350, 214.2156642432025251, 250.0000000000000000 ) ) ;
#2035=AXIS2_PLACEMENT_3D ( 'NONE', #19137, #3501, #2015 ) ;
#2038=EDGE_CURVE ( 'NONE', #13405, #14242, #11939, .T. ) ;
#2039=FILL_AREA_STYLE_COLOUR ( '', #2970 ) ;
#2040=EDGE_CURVE ( 'NONE', #11158, #11636, #4131, .T. ) ;
#2042=DIRECTION ( 'NONE',  ( 1.000000000000000000, -0.000000000000000000, -0.000000000000000000 ) ) ;
#2060=UNCERTAINTY_MEASURE_WITH_UNIT (LENGTH_MEASURE( 1.000000000000000082E-05 ), #15267, 'distance_accuracy_value', 'NONE');
#2068=CARTESIAN_POINT ( 'NONE',  ( 423.8334540492694487, 191.8198460455371333, 158.2339398819845826 ) ) ;
#2069=EDGE_CURVE ( 'NONE', #15261, #13635, #13044, .T. ) ;
#2074=STYLED_ITEM ( 'NONE', ( #1995 ), #18833 ) ;
#2104=DIRECTION ( 'NONE',  ( 0.000000000000000000, -0.000000000000000000, -1.000000000000000000 ) ) ;
#2105=FILL_AREA_STYLE_COLOUR ( '', #6039 ) ;
#2110=FILL_AREA_STYLE ('',( #17579 ) ) ;
#2118=CARTESIAN_POINT ( 'NONE',  ( 423.8334540492694487, 191.8198460455371333, 24.99421986894476078 ) ) ;
#2121=ORIENTED_EDGE ( 'NONE', *, *, #11033, .F. ) ;
#2138=FACE_OUTER_BOUND ( 'NONE', #12205, .T. ) ;
#2156=FACE_OUTER_BOUND ( 'NONE', #1050, .T. ) ;
#2157=CARTESIAN_POINT ( 'NONE',  ( 463.8334540492693350, 191.8198460455371333, 168.2339398819845826 ) ) ;
#2163=ORIENTED_EDGE ( 'NONE', *, *, #10165, .T. ) ;
#2164=EDGE_LOOP ( 'NONE', ( #3428, #16999, #16164, #20184 ) ) ;
#2183=CARTESIAN_POINT ( 'NONE',  ( 498.8117674897343932, 191.8198460455371333, 14.99421986894475012 ) ) ;
#2185=EDGE_CURVE ( 'NONE', #17444, #16566, #8428, .T. ) ;
#2187=ORIENTED_EDGE ( 'NONE', *, *, #9612, .T. ) ;
#2195=CARTESIAN_POINT ( 'NONE',  ( 493.8117674897343363, 214.2156642432025251, 250.0000000000000000 ) ) ;
#2208=ORIENTED_EDGE ( 'NONE', *, *, #12498, .F. ) ;
#2214=SURFACE_STYLE_FILL_AREA ( #3486 ) ;
#2229=( NAMED_UNIT ( * ) PLANE_ANGLE_UNIT ( ) SI_UNIT ( $, .RADIAN. ) );
#2236=LINE ( 'NONE', #11637, #18885 ) ;
#2238=DIRECTION ( 'NONE',  ( -1.000000000000000000, -0.000000000000000000, -0.000000000000000000 ) ) ;
#2247=DIRECTION ( 'NONE',  ( 0.000000000000000000, 0.000000000000000000, 1.000000000000000000 ) ) ;
#2252=DIRECTION ( 'NONE',  ( 1.000000000000000000, 1.197852309262419498E-15, -0.000000000000000000 ) ) ;
#2258=LINE ( 'NONE', #13225, #7908 ) ;
#2263=( GEOMETRIC_REPRESENTATION_CONTEXT ( 3 ) GLOBAL_UNCERTAINTY_ASSIGNED_CONTEXT ( ( #7108 ) ) GLOBAL_UNIT_ASSIGNED_CONTEXT ( ( #13008, #11442, #13114 ) ) REPRESENTATION_CONTEXT ( 'NONE', 'WORKASPACE' ) );
#2269=ORIENTED_EDGE ( 'NONE', *, *, #11172, .F. ) ;
#2308=EDGE_LOOP ( 'NONE', ( #3245, #7438, #18335, #7044 ) ) ;
#2310=EDGE_CURVE ( 'NONE', #13659, #17347, #534, .T. ) ;
#2335=UNCERTAINTY_MEASURE_WITH_UNIT (LENGTH_MEASURE( 1.000000000000000082E-05 ), #7424, 'distance_accuracy_value', 'NONE');
#2336=CARTESIAN_POINT ( 'NONE',  ( 423.8334540492694487, 191.8198460455371333, 168.2339398819845826 ) ) ;
#2348=FACE_BOUND ( 'NONE', #7928, .T. ) ;
#2349=VECTOR ( 'NONE', #12868, 1000.000000000000000 ) ;
#2350=FACE_OUTER_BOUND ( 'NONE', #8991, .T. ) ;
#2357=DIRECTION ( 'NONE',  ( 1.000000000000000000, -0.000000000000000000, -0.000000000000000000 ) ) ;
#2359=( NAMED_UNIT ( * ) PLANE_ANGLE_UNIT ( ) SI_UNIT ( $, .RADIAN. ) );
#2363=EDGE_LOOP ( 'NONE', ( #17108, #13667, #16054, #4191 ) ) ;
#2369=EDGE_CURVE ( 'NONE', #12704, #12426, #14755, .T. ) ;
#2386=DIRECTION ( 'NONE',  ( 1.000000000000000000, 1.197852309262419498E-15, -0.000000000000000000 ) ) ;
#2393=ORIENTED_EDGE ( 'NONE', *, *, #5814, .F. ) ;
#2399=( NAMED_UNIT ( * ) SI_UNIT ( $, .STERADIAN. ) SOLID_ANGLE_UNIT ( ) );
#2403=UNCERTAINTY_MEASURE_WITH_UNIT (LENGTH_MEASURE( 1.000000000000000082E-05 ), #3894, 'distance_accuracy_value', 'NONE');
#2412=FILL_AREA_STYLE_COLOUR ( '', #387 ) ;
#2414=EDGE_CURVE ( 'NONE', #3980, #15201, #11720, .T. ) ;
#2425=VERTEX_POINT ( 'NONE', #14971 ) ;
#2453=ORIENTED_EDGE ( 'NONE', *, *, #10898, .F. ) ;
#2460=AXIS2_PLACEMENT_3D ( 'NONE', #5180, #16506, #2247 ) ;
#2463=CYLINDRICAL_SURFACE ( 'NONE', #14121, 10.00000000000000888 ) ;
#2473=( LENGTH_UNIT ( ) NAMED_UNIT ( * ) SI_UNIT ( .MILLI., .METRE. ) );
#2481=PLANE ( 'NONE',  #8412 ) ;
#2484=( GEOMETRIC_REPRESENTATION_CONTEXT ( 3 ) GLOBAL_UNCERTAINTY_ASSIGNED_CONTEXT ( ( #11217 ) ) GLOBAL_UNIT_ASSIGNED_CONTEXT ( ( #17449, #17358, #14261 ) ) REPRESENTATION_CONTEXT ( 'NONE', 'WORKASPACE' ) );
#2497=ADVANCED_FACE ( 'NONE', ( #7449 ), #18749, .F. ) ;
#2499=FILL_AREA_STYLE_COLOUR ( '', #293 ) ;
#2511=ORIENTED_EDGE ( 'NONE', *, *, #19315, .F. ) ;
#2512=CARTESIAN_POINT ( 'NONE',  ( 498.8117674897343932, 191.8198460455371333, 24.99421986894476078 ) ) ;
#2514=FILL_AREA_STYLE ('',( #10349 ) ) ;
#2522=EDGE_CURVE ( 'NONE', #8848, #7492, #3167, .T. ) ;
#2523=FACE_OUTER_BOUND ( 'NONE', #16520, .T. ) ;
#2529=ORIENTED_EDGE ( 'NONE', *, *, #18180, .F. ) ;
#2535=DIRECTION ( 'NONE',  ( 1.000000000000000000, 0.000000000000000000, -0.000000000000000000 ) ) ;
#2550=EDGE_LOOP ( 'NONE', ( #18379, #12059 ) ) ;
#2554=SURFACE_SIDE_STYLE ('',( #19648 ) ) ;
#2564=SURFACE_SIDE_STYLE ('',( #7618 ) ) ;
#2577=SURFACE_SIDE_STYLE ('',( #18241 ) ) ;
#2607=SURFACE_SIDE_STYLE ('',( #8899 ) ) ;
#2610=LINE ( 'NONE', #10449, #4751 ) ;
#2641=( NAMED_UNIT ( * ) PLANE_ANGLE_UNIT ( ) SI_UNIT ( $, .RADIAN. ) );
#2644=PRESENTATION_STYLE_ASSIGNMENT (( #12225 ) ) ;
#2657=PLANE ( 'NONE',  #14615 ) ;
#2665=FILL_AREA_STYLE_COLOUR ( '', #13813 ) ;
#2671=STYLED_ITEM ( 'NONE', ( #6086 ), #17188 ) ;
#2679=UNCERTAINTY_MEASURE_WITH_UNIT (LENGTH_MEASURE( 1.000000000000000082E-05 ), #20149, 'distance_accuracy_value', 'NONE');
#2681=( NAMED_UNIT ( * ) PLANE_ANGLE_UNIT ( ) SI_UNIT ( $, .RADIAN. ) );
#2689=DIRECTION ( 'NONE',  ( 1.000000000000000000, 0.000000000000000000, -0.000000000000000000 ) ) ;
#2709=COLOUR_RGB ( '', 0.66274510, 0.83137255, 0.94901961) ;
#2710=DIRECTION ( 'NONE',  ( -0.000000000000000000, -0.000000000000000000, -1.000000000000000000 ) ) ;
#2715=( GEOMETRIC_REPRESENTATION_CONTEXT ( 3 ) GLOBAL_UNCERTAINTY_ASSIGNED_CONTEXT ( ( #621 ) ) GLOBAL_UNIT_ASSIGNED_CONTEXT ( ( #1117, #18446, #13726 ) ) REPRESENTATION_CONTEXT ( 'NONE', 'WORKASPACE' ) );
#2721=VECTOR ( 'NONE', #16255, 1000.000000000000000 ) ;
#2741=AXIS2_PLACEMENT_3D ( 'NONE', #5042, #3500, #8234 ) ;
#2749=MECHANICAL_DESIGN_GEOMETRIC_PRESENTATION_REPRESENTATION('',(#4399),#7381);
#2764=DIRECTION ( 'NONE',  ( 1.000000000000000000, 0.000000000000000000, -0.000000000000000000 ) ) ;
#2767=FILL_AREA_STYLE_COLOUR ( '', #15846 ) ;
#2773=STYLED_ITEM ( 'NONE', ( #11963 ), #19583 ) ;
#2777=MECHANICAL_DESIGN_GEOMETRIC_PRESENTATION_REPRESENTATION('',(#6756),#14306);
#2786=COLOUR_RGB ( '', 0.40784314, 0.44705882, 0.49803922) ;
#2787=DIRECTION ( 'NONE',  ( 1.000000000000000000, -0.000000000000000000, -0.000000000000000000 ) ) ;
#2795=CARTESIAN_POINT ( 'NONE',  ( 463.8334540492693350, 191.8198460455371333, 168.2339398819845826 ) ) ;
#2804=ORIENTED_EDGE ( 'NONE', *, *, #4709, .T. ) ;
#2809=AXIS2_PLACEMENT_3D ( 'NONE', #8873, #5388, #5576 ) ;
#2810=CARTESIAN_POINT ( 'NONE',  ( 423.8334540492694487, 191.8198460455371333, 168.2339398819845826 ) ) ;
#2834=CARTESIAN_POINT ( 'NONE',  ( 468.8334540492694487, 214.2156642432025251, 245.0000000000000000 ) ) ;
#2842=CARTESIAN_POINT ( 'NONE',  ( 498.8334540492693918, 191.8198460455371333, 168.2339398819845826 ) ) ;
#2844=CIRCLE ( 'NONE', #18647, 10.00000000000000888 ) ;
#2846=CARTESIAN_POINT ( 'NONE',  ( 423.8334540492694487, 191.8198460455371333, 91.76606011801541740 ) ) ;
#2849=DIRECTION ( 'NONE',  ( 1.000000000000000000, 0.000000000000000000, 0.000000000000000000 ) ) ;
#2859=FACE_BOUND ( 'NONE', #15325, .T. ) ;
#2864=EDGE_CURVE ( 'NONE', #3254, #4150, #10418, .T. ) ;
#2872=VERTEX_POINT ( 'NONE', #10408 ) ;
#2880=UNCERTAINTY_MEASURE_WITH_UNIT (LENGTH_MEASURE( 1.000000000000000082E-05 ), #3697, 'distance_accuracy_value', 'NONE');
#2895=AXIS2_PLACEMENT_3D ( 'NONE', #3968, #8310, #14583 ) ;
#2915=CARTESIAN_POINT ( 'NONE',  ( 498.8117674897343932, 134.2156642432025251, -87.31255586191144857 ) ) ;
#2919=AXIS2_PLACEMENT_3D ( 'NONE', #13074, #13369, #14883 ) ;
#2929=CARTESIAN_POINT ( 'NONE',  ( 463.8334540492693350, 191.8198460455371333, 178.2339398819846110 ) ) ;
#2939=( LENGTH_UNIT ( ) NAMED_UNIT ( * ) SI_UNIT ( .MILLI., .METRE. ) );
#2940=LINE ( 'NONE', #10579, #4051 ) ;
#2960=DIRECTION ( 'NONE',  ( 1.000000000000000000, -0.000000000000000000, -0.000000000000000000 ) ) ;
#2962=FILL_AREA_STYLE ('',( #20278 ) ) ;
#2970=COLOUR_RGB ( '', 0.40784314, 0.44705882, 0.49803922) ;
#2991=CARTESIAN_POINT ( 'NONE',  ( 463.8334540492693350, 214.2156642432025251, 250.0000000000000000 ) ) ;
#2997=STYLED_ITEM ( 'NONE', ( #3096 ), #7742 ) ;
#2999=ORIENTED_EDGE ( 'NONE', *, *, #17055, .T. ) ;
#3016=DIRECTION ( 'NONE',  ( -0.000000000000000000, 0.000000000000000000, -1.000000000000000000 ) ) ;
#3021=VECTOR ( 'NONE', #10865, 1000.000000000000000 ) ;
#3035=CARTESIAN_POINT ( 'NONE',  ( 463.8334540492693350, 191.8198460455371333, 24.99421986894476078 ) ) ;
#3040=( NAMED_UNIT ( * ) PLANE_ANGLE_UNIT ( ) SI_UNIT ( $, .RADIAN. ) );
#3054=PRESENTATION_STYLE_ASSIGNMENT (( #11199 ) ) ;
#3062=EDGE_LOOP ( 'NONE', ( #6024, #11843 ) ) ;
#3063=SURFACE_STYLE_FILL_AREA ( #7717 ) ;
#3068=CARTESIAN_POINT ( 'NONE',  ( 463.8334540492693350, 191.8198460455371333, 91.76606011801541740 ) ) ;
#3087=CIRCLE ( 'NONE', #8024, 10.00000000000000888 ) ;
#3088=AXIS2_PLACEMENT_3D ( 'NONE', #15624, #3016, #18880 ) ;
#3090=DIRECTION ( 'NONE',  ( 0.000000000000000000, 0.000000000000000000, -1.000000000000000000 ) ) ;
#3091=COLOUR_RGB ( '', 0.66274510, 0.83137255, 0.94901961) ;
#3095=STYLED_ITEM ( 'NONE', ( #165 ), #15540 ) ;
#3096=PRESENTATION_STYLE_ASSIGNMENT (( #3200 ) ) ;
#3101=DIRECTION ( 'NONE',  ( 0.000000000000000000, 0.000000000000000000, -1.000000000000000000 ) ) ;
#3111=VECTOR ( 'NONE', #2042, 1000.000000000000000 ) ;
#3119=ORIENTED_EDGE ( 'NONE', *, *, #19651, .F. ) ;
#3128=DIRECTION ( 'NONE',  ( -1.000000000000000000, 0.000000000000000000, 0.000000000000000000 ) ) ;
#3135=AXIS2_PLACEMENT_3D ( 'NONE', #2834, #4093, #961 ) ;
#3144=DIRECTION ( 'NONE',  ( -0.000000000000000000, 0.000000000000000000, 1.000000000000000000 ) ) ;
#3162=DIRECTION ( 'NONE',  ( 1.000000000000000000, 0.000000000000000000, -0.000000000000000000 ) ) ;
#3165=FILL_AREA_STYLE_COLOUR ( '', #9019 ) ;
#3167=CIRCLE ( 'NONE', #4470, 10.00000000000001066 ) ;
#3171=( NAMED_UNIT ( * ) PLANE_ANGLE_UNIT ( ) SI_UNIT ( $, .RADIAN. ) );
#3200=SURFACE_STYLE_USAGE ( .BOTH. , #19041 ) ;
#3210=DIRECTION ( 'NONE',  ( 0.000000000000000000, 0.000000000000000000, -1.000000000000000000 ) ) ;
#3213=EDGE_CURVE ( 'NONE', #11216, #6215, #18159, .T. ) ;
#3224=LINE ( 'NONE', #1330, #4405 ) ;
#3240=ORIENTED_EDGE ( 'NONE', *, *, #13768, .T. ) ;
#3245=ORIENTED_EDGE ( 'NONE', *, *, #10134, .F. ) ;
#3253=FILL_AREA_STYLE ('',( #156 ) ) ;
#3254=VERTEX_POINT ( 'NONE', #15116 ) ;
#3257=DIRECTION ( 'NONE',  ( 1.000000000000000000, 0.000000000000000000, 0.000000000000000000 ) ) ;
#3273=FILL_AREA_STYLE ('',( #69 ) ) ;
#3275=CIRCLE ( 'NONE', #13801, 10.00000000000000888 ) ;
#3297=DIRECTION ( 'NONE',  ( 0.000000000000000000, 0.000000000000000000, -1.000000000000000000 ) ) ;
#3317=PRESENTATION_STYLE_ASSIGNMENT (( #14049 ) ) ;
#3344=EDGE_CURVE ( 'NONE', #8331, #8375, #10879, .T. ) ;
#3345=COLOUR_RGB ( '', 0.08235294, 0.09019608, 0.10196078) ;
#3361=DIRECTION ( 'NONE',  ( 0.000000000000000000, -1.000000000000000000, 0.000000000000000000 ) ) ;
#3371=SURFACE_STYLE_USAGE ( .BOTH. , #4518 ) ;
#3396=MECHANICAL_DESIGN_GEOMETRIC_PRESENTATION_REPRESENTATION('',(#9634),#14865);
#3397=ORIENTED_EDGE ( 'NONE', *, *, #5756, .T. ) ;
#3399=EDGE_LOOP ( 'NONE', ( #2269, #19922, #1471, #12921 ) ) ;
#3400=UNCERTAINTY_MEASURE_WITH_UNIT (LENGTH_MEASURE( 1.000000000000000082E-05 ), #11505, 'distance_accuracy_value', 'NONE');
#3406=FILL_AREA_STYLE ('',( #17500 ) ) ;
#3413=FILL_AREA_STYLE_COLOUR ( '', #2709 ) ;
#3428=ORIENTED_EDGE ( 'NONE', *, *, #14826, .F. ) ;
#3434=FILL_AREA_STYLE_COLOUR ( '', #734 ) ;
#3440=DIRECTION ( 'NONE',  ( 1.000000000000000000, -0.000000000000000000, -0.000000000000000000 ) ) ;
#3459=FACE_OUTER_BOUND ( 'NONE', #16103, .T. ) ;
#3462=LINE ( 'NONE', #19311, #7553 ) ;
#3481=VERTEX_POINT ( 'NONE', #838 ) ;
#3486=FILL_AREA_STYLE ('',( #479 ) ) ;
#3490=FACE_OUTER_BOUND ( 'NONE', #2308, .T. ) ;
#3500=DIRECTION ( 'NONE',  ( 0.000000000000000000, 0.000000000000000000, 1.000000000000000000 ) ) ;
#3501=DIRECTION ( 'NONE',  ( 1.000000000000000000, 0.000000000000000000, -0.000000000000000000 ) ) ;
#3517=SURFACE_STYLE_FILL_AREA ( #9795 ) ;
#3524=FILL_AREA_STYLE ('',( #2039 ) ) ;
#3556=CARTESIAN_POINT ( 'NONE',  ( 498.8117674897343932, 191.8198460455371333, 81.76606011801540319 ) ) ;
#3563=EDGE_CURVE ( 'NONE', #11798, #7874, #7542, .T. ) ;
#3564=LINE ( 'NONE', #8204, #2721 ) ;
#3576=DIRECTION ( 'NONE',  ( 0.000000000000000000, 0.000000000000000000, -1.000000000000000000 ) ) ;
#3579=CIRCLE ( 'NONE', #17719, 10.00000000000001066 ) ;
#3580=ORIENTED_EDGE ( 'NONE', *, *, #3671, .F. ) ;
#3582=DIRECTION ( 'NONE',  ( 1.000000000000000000, -0.000000000000000000, -0.000000000000000000 ) ) ;
#3594=DIRECTION ( 'NONE',  ( 1.000000000000000000, -0.000000000000000000, -0.000000000000000000 ) ) ;
#3602=LINE ( 'NONE', #14723, #10234 ) ;
#3609=STYLED_ITEM ( 'NONE', ( #18162 ), #11043 ) ;
#3614=CARTESIAN_POINT ( 'NONE',  ( 498.8334540492693918, 214.2156642432025251, 250.0000000000000000 ) ) ;
#3619=( GEOMETRIC_REPRESENTATION_CONTEXT ( 3 ) GLOBAL_UNCERTAINTY_ASSIGNED_CONTEXT ( ( #6837 ) ) GLOBAL_UNIT_ASSIGNED_CONTEXT ( ( #2473, #19761, #18229 ) ) REPRESENTATION_CONTEXT ( 'NONE', 'WORKASPACE' ) );
#3642=( NAMED_UNIT ( * ) SI_UNIT ( $, .STERADIAN. ) SOLID_ANGLE_UNIT ( ) );
#3652=CARTESIAN_POINT ( 'NONE',  ( 503.8334540492693918, 242.8734308960556234, 0.000000000000000000 ) ) ;
#3665=SURFACE_STYLE_USAGE ( .BOTH. , #9845 ) ;
#3667=ORIENTED_EDGE ( 'NONE', *, *, #1737, .F. ) ;
#3671=EDGE_CURVE ( 'NONE', #12734, #6007, #4650, .T. ) ;
#3674=EDGE_LOOP ( 'NONE', ( #6199, #8988, #15111, #19349, #5136, #18507, #19814, #6846 ) ) ;
#3685=EDGE_CURVE ( 'NONE', #4282, #664, #14034, .T. ) ;
#3697=( LENGTH_UNIT ( ) NAMED_UNIT ( * ) SI_UNIT ( .MILLI., .METRE. ) );
#3718=EDGE_CURVE ( 'NONE', #7492, #7254, #9577, .T. ) ;
#3736=UNCERTAINTY_MEASURE_WITH_UNIT (LENGTH_MEASURE( 1.000000000000000082E-05 ), #8161, 'distance_accuracy_value', 'NONE');
#3739=ORIENTED_EDGE ( 'NONE', *, *, #12267, .F. ) ;
#3740=EDGE_CURVE ( 'NONE', #6449, #5650, #18961, .T. ) ;
#3745=FILL_AREA_STYLE ('',( #633 ) ) ;
#3759=UNCERTAINTY_MEASURE_WITH_UNIT (LENGTH_MEASURE( 1.000000000000000082E-05 ), #7160, 'distance_accuracy_value', 'NONE');
#3787=DIRECTION ( 'NONE',  ( 0.000000000000000000, 0.000000000000000000, -1.000000000000000000 ) ) ;
#3799=CIRCLE ( 'NONE', #11365, 10.00000000000000888 ) ;
#3800=DIRECTION ( 'NONE',  ( -1.000000000000000000, 0.000000000000000000, 0.000000000000000000 ) ) ;
#3807=DIRECTION ( 'NONE',  ( 0.000000000000000000, 0.000000000000000000, 1.000000000000000000 ) ) ;
#3814=ORIENTED_EDGE ( 'NONE', *, *, #15974, .T. ) ;
#3821=PRESENTATION_STYLE_ASSIGNMENT (( #5556 ) ) ;
#3822=MECHANICAL_DESIGN_GEOMETRIC_PRESENTATION_REPRESENTATION('',(#1139),#5810);
#3829=PLANE ( 'NONE',  #7397 ) ;
#3831=EDGE_CURVE ( 'NONE', #8449, #19193, #11545, .T. ) ;
#3832=ORIENTED_EDGE ( 'NONE', *, *, #3563, .T. ) ;
#3833=CIRCLE ( 'NONE', #20275, 10.00000000000000888 ) ;
#3834=ORIENTED_EDGE ( 'NONE', *, *, #11303, .F. ) ;
#3837=VERTEX_POINT ( 'NONE', #7021 ) ;
#3853=ORIENTED_EDGE ( 'NONE', *, *, #17964, .F. ) ;
#3894=( LENGTH_UNIT ( ) NAMED_UNIT ( * ) SI_UNIT ( .MILLI., .METRE. ) );
#3911=DIRECTION ( 'NONE',  ( -0.000000000000000000, 0.000000000000000000, -1.000000000000000000 ) ) ;
#3914=CARTESIAN_POINT ( 'NONE',  ( 503.8334540492693918, 191.8198460455371333, 225.0057801310552463 ) ) ;
#3915=CARTESIAN_POINT ( 'NONE',  ( 423.8334540492694487, 191.8198460455371333, 14.99421986894475012 ) ) ;
#3919=( GEOMETRIC_REPRESENTATION_CONTEXT ( 3 ) GLOBAL_UNCERTAINTY_ASSIGNED_CONTEXT ( ( #12686 ) ) GLOBAL_UNIT_ASSIGNED_CONTEXT ( ( #16546, #16161, #1988 ) ) REPRESENTATION_CONTEXT ( 'NONE', 'WORKASPACE' ) );
#3922=SURFACE_STYLE_USAGE ( .BOTH. , #11767 ) ;
#3936=STYLED_ITEM ( 'NONE', ( #3821 ), #6510 ) ;
#3947=AXIS2_PLACEMENT_3D ( 'NONE', #6586, #14302, #1908 ) ;
#3960=SURFACE_STYLE_USAGE ( .BOTH. , #15090 ) ;
#3968=CARTESIAN_POINT ( 'NONE',  ( 503.8334540492693918, 191.8198460455371333, 24.99421986894476078 ) ) ;
#3980=VERTEX_POINT ( 'NONE', #3068 ) ;
#3988=CARTESIAN_POINT ( 'NONE',  ( 463.8334540492693350, 191.8198460455371333, 71.76606011801538898 ) ) ;
#3992=STYLED_ITEM ( 'NONE', ( #2644 ), #17431 ) ;
#3993=LINE ( 'NONE', #2846, #7748 ) ;
#3994=AXIS2_PLACEMENT_3D ( 'NONE', #6408, #11128, #3297 ) ;
#3997=UNCERTAINTY_MEASURE_WITH_UNIT (LENGTH_MEASURE( 1.000000000000000082E-05 ), #9155, 'distance_accuracy_value', 'NONE');
#4007=DIRECTION ( 'NONE',  ( 1.000000000000000000, 0.000000000000000000, 0.000000000000000000 ) ) ;
#4020=CIRCLE ( 'NONE', #7318, 10.00000000000000888 ) ;
#4030=( NAMED_UNIT ( * ) SI_UNIT ( $, .STERADIAN. ) SOLID_ANGLE_UNIT ( ) );
#4051=VECTOR ( 'NONE', #16879, 1000.000000000000000 ) ;
#4064=DIRECTION ( 'NONE',  ( 0.000000000000000000, 0.000000000000000000, -1.000000000000000000 ) ) ;
#4070=EDGE_CURVE ( 'NONE', #11158, #18080, #17189, .T. ) ;
#4076=AXIS2_PLACEMENT_3D ( 'NONE', #9326, #148, #6455 ) ;
#4084=AXIS2_PLACEMENT_3D ( 'NONE', #16286, #3594, #17484 ) ;
#4093=DIRECTION ( 'NONE',  ( -1.000000000000000000, 0.000000000000000000, -0.000000000000000000 ) ) ;
#4094=FACE_OUTER_BOUND ( 'NONE', #3399, .T. ) ;
#4106=COLOUR_RGB ( '', 0.31764706, 0.68627451, 0.89019608) ;
#4129=DIRECTION ( 'NONE',  ( 1.000000000000000000, -0.000000000000000000, -0.000000000000000000 ) ) ;
#4131=CIRCLE ( 'NONE', #14313, 10.00000000000000888 ) ;
#4136=VECTOR ( 'NONE', #13790, 1000.000000000000000 ) ;
#4138=FILL_AREA_STYLE ('',( #2665 ) ) ;
#4149=DIRECTION ( 'NONE',  ( -1.197852309262419498E-15, 1.000000000000000000, 0.000000000000000000 ) ) ;
#4150=VERTEX_POINT ( 'NONE', #14406 ) ;
#4152=DIRECTION ( 'NONE',  ( 0.000000000000000000, 0.000000000000000000, -1.000000000000000000 ) ) ;
#4172=EDGE_LOOP ( 'NONE', ( #2453, #8455 ) ) ;
#4173=UNCERTAINTY_MEASURE_WITH_UNIT (LENGTH_MEASURE( 1.000000000000000082E-05 ), #17002, 'distance_accuracy_value', 'NONE');
#4182=( LENGTH_UNIT ( ) NAMED_UNIT ( * ) SI_UNIT ( .MILLI., .METRE. ) );
#4191=ORIENTED_EDGE ( 'NONE', *, *, #19435, .F. ) ;
#4199=ORIENTED_EDGE ( 'NONE', *, *, #2040, .T. ) ;
#4200=SURFACE_STYLE_USAGE ( .BOTH. , #9128 ) ;
#4204=CARTESIAN_POINT ( 'NONE',  ( 493.8117674897343363, 214.2156642432025251, 245.0000000000000000 ) ) ;
#4240=FACE_BOUND ( 'NONE', #6707, .T. ) ;
#4248=DIRECTION ( 'NONE',  ( 1.000000000000000000, 0.000000000000000000, 0.000000000000000000 ) ) ;
#4259=COLOUR_RGB ( '', 0.72549020, 0.75294118, 0.79215686) ;
#4269=( NAMED_UNIT ( * ) SI_UNIT ( $, .STERADIAN. ) SOLID_ANGLE_UNIT ( ) );
#4282=VERTEX_POINT ( 'NONE', #18092 ) ;
#4283=ORIENTED_EDGE ( 'NONE', *, *, #1258, .T. ) ;
#4290=AXIS2_PLACEMENT_3D ( 'NONE', #7064, #13361, #11274 ) ;
#4311=CARTESIAN_POINT ( 'NONE',  ( 486.8117674897343363, 214.2156642432025251, 250.0000000000000000 ) ) ;
#4312=CARTESIAN_POINT ( 'NONE',  ( 463.8334540492693350, 214.2156642432025251, 250.0000000000000000 ) ) ;
#4314=CARTESIAN_POINT ( 'NONE',  ( 463.8334540492693350, 134.2156642432025251, 0.000000000000000000 ) ) ;
#4317=CARTESIAN_POINT ( 'NONE',  ( 423.8334540492694487, 191.8198460455371333, 14.99421986894475012 ) ) ;
#4330=ORIENTED_EDGE ( 'NONE', *, *, #15909, .T. ) ;
#4331=DIRECTION ( 'NONE',  ( 0.000000000000000000, 0.000000000000000000, -1.000000000000000000 ) ) ;
#4334=( NAMED_UNIT ( * ) PLANE_ANGLE_UNIT ( ) SI_UNIT ( $, .RADIAN. ) );
#4336=DIRECTION ( 'NONE',  ( -0.000000000000000000, 0.000000000000000000, 1.000000000000000000 ) ) ;
#4337=UNCERTAINTY_MEASURE_WITH_UNIT (LENGTH_MEASURE( 1.000000000000000082E-05 ), #19870, 'distance_accuracy_value', 'NONE');
#4341=DIRECTION ( 'NONE',  ( 1.000000000000000000, 0.000000000000000000, -0.000000000000000000 ) ) ;
#4347=DIRECTION ( 'NONE',  ( -1.000000000000000000, 0.000000000000000000, 0.000000000000000000 ) ) ;
#4350=( NAMED_UNIT ( * ) PLANE_ANGLE_UNIT ( ) SI_UNIT ( $, .RADIAN. ) );
#4357=EDGE_LOOP ( 'NONE', ( #15310, #1202 ) ) ;
#4358=CARTESIAN_POINT ( 'NONE',  ( 463.8334540492693350, 134.2156642432025251, 250.0000000000000000 ) ) ;
#4382=DIRECTION ( 'NONE',  ( 0.000000000000000000, 0.000000000000000000, -1.000000000000000000 ) ) ;
#4384=CARTESIAN_POINT ( 'NONE',  ( 498.8334540492693918, 191.8198460455371333, 215.0057801310552179 ) ) ;
#4387=DIRECTION ( 'NONE',  ( 0.000000000000000000, 0.000000000000000000, -1.000000000000000000 ) ) ;
#4399=STYLED_ITEM ( 'NONE', ( #9554 ), #12216 ) ;
#4405=VECTOR ( 'NONE', #7658, 1000.000000000000000 ) ;
#4407=STYLED_ITEM ( 'NONE', ( #19880 ), #239 ) ;
#4416=SURFACE_STYLE_USAGE ( .BOTH. , #18519 ) ;
#4431=ORIENTED_EDGE ( 'NONE', *, *, #3213, .F. ) ;
#4470=AXIS2_PLACEMENT_3D ( 'NONE', #15483, #4341, #18545 ) ;
#4491=AXIS2_PLACEMENT_3D ( 'NONE', #8538, #8642, #17918 ) ;
#4514=EDGE_CURVE ( 'NONE', #17286, #12308, #8926, .T. ) ;
#4518=SURFACE_SIDE_STYLE ('',( #176 ) ) ;
#4522=LINE ( 'NONE', #9356, #11629 ) ;
#4524=FILL_AREA_STYLE_COLOUR ( '', #18392 ) ;
#4536=ORIENTED_EDGE ( 'NONE', *, *, #13056, .T. ) ;
#4565=DIRECTION ( 'NONE',  ( 1.000000000000000000, 0.000000000000000000, -0.000000000000000000 ) ) ;
#4570=LINE ( 'NONE', #124, #19978 ) ;
#4575=PRESENTATION_STYLE_ASSIGNMENT (( #10859 ) ) ;
#4584=VECTOR ( 'NONE', #6873, 1000.000000000000000 ) ;
#4585=EDGE_LOOP ( 'NONE', ( #9679, #14488, #17716, #15474 ) ) ;
#4600=CARTESIAN_POINT ( 'NONE',  ( 463.8334540492693350, 134.2156642432025251, 250.0000000000000000 ) ) ;
#4601=ORIENTED_EDGE ( 'NONE', *, *, #12544, .T. ) ;
#4603=CARTESIAN_POINT ( 'NONE',  ( 475.8334540492694487, 214.2156642432025251, 245.0000000000000000 ) ) ;
#4619=DIRECTION ( 'NONE',  ( 1.000000000000000000, 0.000000000000000000, 0.000000000000000000 ) ) ;
#4625=MECHANICAL_DESIGN_GEOMETRIC_PRESENTATION_REPRESENTATION('',(#9218),#16799);
#4640=EDGE_CURVE ( 'NONE', #1837, #20367, #12793, .T. ) ;
#4645=CARTESIAN_POINT ( 'NONE',  ( 498.8117674897343932, 191.8198460455371333, 24.99421986894476078 ) ) ;
#4650=LINE ( 'NONE', #6106, #89 ) ;
#4652=CARTESIAN_POINT ( 'NONE',  ( 458.8334540492693350, 191.8198460455371333, 215.0057801310552179 ) ) ;
#4659=CARTESIAN_POINT ( 'NONE',  ( 423.8334540492694487, 191.8198460455371333, 235.0057801310552463 ) ) ;
#4661=CARTESIAN_POINT ( 'NONE',  ( 498.8334540492693918, 214.2156642432025251, 250.0000000000000000 ) ) ;
#4693=( LENGTH_UNIT ( ) NAMED_UNIT ( * ) SI_UNIT ( .MILLI., .METRE. ) );
#4695=EDGE_CURVE ( 'NONE', #15257, #7254, #18367, .T. ) ;
#4701=PLANE ( 'NONE',  #14961 ) ;
#4709=EDGE_CURVE ( 'NONE', #664, #8243, #6968, .T. ) ;
#4722=FACE_BOUND ( 'NONE', #4357, .T. ) ;
#4733=EDGE_CURVE ( 'NONE', #13911, #6449, #11808, .T. ) ;
#4735=CARTESIAN_POINT ( 'NONE',  ( 0.000000000000000000, 0.000000000000000000, 250.0000000000000000 ) ) ;
#4751=VECTOR ( 'NONE', #2710, 1000.000000000000000 ) ;
#4760=DIRECTION ( 'NONE',  ( -0.000000000000000000, -0.000000000000000000, 1.000000000000000000 ) ) ;
#4762=FACE_OUTER_BOUND ( 'NONE', #19992, .T. ) ;
#4768=MECHANICAL_DESIGN_GEOMETRIC_PRESENTATION_REPRESENTATION('',(#2773),#19240);
#4777=ORIENTED_EDGE ( 'NONE', *, *, #18946, .F. ) ;
#4795=ORIENTED_EDGE ( 'NONE', *, *, #18429, .F. ) ;
#4804=CARTESIAN_POINT ( 'NONE',  ( 458.8334540492693350, 191.8198460455371333, 81.76606011801540319 ) ) ;
#4817=SHAPE_REPRESENTATION_RELATIONSHIP ( 'NONE' , 'NONE' ,  #6180, #1492 ) ;
#4821=ORIENTED_EDGE ( 'NONE', *, *, #6278, .F. ) ;
#4825=EDGE_CURVE ( 'NONE', #13802, #2872, #3579, .T. ) ;
#4830=AXIS2_PLACEMENT_3D ( 'NONE', #7518, #986, #7610 ) ;
#4843=( LENGTH_UNIT ( ) NAMED_UNIT ( * ) SI_UNIT ( .MILLI., .METRE. ) );
#4844=SURFACE_STYLE_USAGE ( .BOTH. , #10813 ) ;
#4847=ORIENTED_EDGE ( 'NONE', *, *, #14530, .T. ) ;
#4882=ORIENTED_EDGE ( 'NONE', *, *, #476, .T. ) ;
#4884=DIRECTION ( 'NONE',  ( -0.000000000000000000, -0.000000000000000000, 1.000000000000000000 ) ) ;
#4895=LINE ( 'NONE', #11389, #16620 ) ;
#4922=STYLED_ITEM ( 'NONE', ( #10706 ), #6592 ) ;
#4927=MECHANICAL_DESIGN_GEOMETRIC_PRESENTATION_REPRESENTATION('',(#8066),#11847);
#4969=CARTESIAN_POINT ( 'NONE',  ( 503.8334540492693918, 0.000000000000000000, 0.000000000000000000 ) ) ;
#4972=DIRECTION ( 'NONE',  ( 1.000000000000000000, -0.000000000000000000, -0.000000000000000000 ) ) ;
#5002=AXIS2_PLACEMENT_3D ( 'NONE', #8218, #3582, #3787 ) ;
#5006=DIRECTION ( 'NONE',  ( -0.000000000000000000, 1.000000000000000000, -0.000000000000000000 ) ) ;
#5017=STYLED_ITEM ( 'NONE', ( #10251 ), #17816 ) ;
#5019=( LENGTH_UNIT ( ) NAMED_UNIT ( * ) SI_UNIT ( .MILLI., .METRE. ) );
#5042=CARTESIAN_POINT ( 'NONE',  ( 0.000000000000000000, 0.000000000000000000, 0.000000000000000000 ) ) ;
#5051=UNCERTAINTY_MEASURE_WITH_UNIT (LENGTH_MEASURE( 1.000000000000000082E-05 ), #7262, 'distance_accuracy_value', 'NONE');
#5068=SURFACE_STYLE_USAGE ( .BOTH. , #16020 ) ;
#5087=PLANE ( 'NONE',  #5369 ) ;
#5090=LINE ( 'NONE', #18041, #16337 ) ;
#5110=ORIENTED_EDGE ( 'NONE', *, *, #12544, .F. ) ;
#5114=ORIENTED_EDGE ( 'NONE', *, *, #11309, .F. ) ;
#5118=ADVANCED_FACE ( 'NONE', ( #20097 ), #7249, .T. ) ;
#5119=LINE ( 'NONE', #2195, #18211 ) ;
#5136=ORIENTED_EDGE ( 'NONE', *, *, #7859, .T. ) ;
#5166=ORIENTED_EDGE ( 'NONE', *, *, #3685, .F. ) ;
#5170=PRESENTATION_STYLE_ASSIGNMENT (( #8540 ) ) ;
#5180=CARTESIAN_POINT ( 'NONE',  ( 463.8334540492693350, 191.8198460455371333, 225.0057801310552463 ) ) ;
#5192=UNCERTAINTY_MEASURE_WITH_UNIT (LENGTH_MEASURE( 1.000000000000000082E-05 ), #13425, 'distance_accuracy_value', 'NONE');
#5198=( LENGTH_UNIT ( ) NAMED_UNIT ( * ) SI_UNIT ( .MILLI., .METRE. ) );
#5225=ORIENTED_EDGE ( 'NONE', *, *, #10154, .T. ) ;
#5271=CARTESIAN_POINT ( 'NONE',  ( 423.8334540492694487, 191.8198460455371333, 24.99421986894476078 ) ) ;
#5301=AXIS2_PLACEMENT_3D ( 'NONE', #10128, #19479, #13045 ) ;
#5323=EDGE_LOOP ( 'NONE', ( #15311, #2163 ) ) ;
#5334=CARTESIAN_POINT ( 'NONE',  ( 423.8334540492694487, 191.8198460455371333, 81.76606011801540319 ) ) ;
#5360=SURFACE_SIDE_STYLE ('',( #16106 ) ) ;
#5369=AXIS2_PLACEMENT_3D ( 'NONE', #15270, #7541, #12170 ) ;
#5376=SURFACE_STYLE_FILL_AREA ( #19460 ) ;
#5377=VECTOR ( 'NONE', #12581, 1000.000000000000000 ) ;
#5380=UNCERTAINTY_MEASURE_WITH_UNIT (LENGTH_MEASURE( 1.000000000000000082E-05 ), #266, 'distance_accuracy_value', 'NONE');
#5382=CIRCLE ( 'NONE', #6770, 10.00000000000000888 ) ;
#5388=DIRECTION ( 'NONE',  ( -1.000000000000000000, 0.000000000000000000, 0.000000000000000000 ) ) ;
#5390=CARTESIAN_POINT ( 'NONE',  ( 498.8334540492693918, 214.2156642432025251, 0.000000000000000000 ) ) ;
#5401=MECHANICAL_DESIGN_GEOMETRIC_PRESENTATION_REPRESENTATION('',(#2074),#1397);
#5409=FACE_BOUND ( 'NONE', #1833, .T. ) ;
#5411=CARTESIAN_POINT ( 'NONE',  ( 423.8334540492694487, 191.8198460455371333, 235.0057801310552463 ) ) ;
#5424=( NAMED_UNIT ( * ) SI_UNIT ( $, .STERADIAN. ) SOLID_ANGLE_UNIT ( ) );
#5431=COLOUR_RGB ( '', 0.66274510, 0.83137255, 0.94901961) ;
#5453=UNCERTAINTY_MEASURE_WITH_UNIT (LENGTH_MEASURE( 1.000000000000000082E-05 ), #20315, 'distance_accuracy_value', 'NONE');
#5460=EDGE_LOOP ( 'NONE', ( #9623, #6065, #3832, #9650 ) ) ;
#5472=SURFACE_STYLE_FILL_AREA ( #3524 ) ;
#5474=DIRECTION ( 'NONE',  ( 0.000000000000000000, 0.000000000000000000, -1.000000000000000000 ) ) ;
#5481=FACE_BOUND ( 'NONE', #7482, .T. ) ;
#5522=SURFACE_STYLE_FILL_AREA ( #8504 ) ;
#5545=FACE_OUTER_BOUND ( 'NONE', #7620, .T. ) ;
#5549=UNCERTAINTY_MEASURE_WITH_UNIT (LENGTH_MEASURE( 1.000000000000000082E-05 ), #5019, 'distance_accuracy_value', 'NONE');
#5556=SURFACE_STYLE_USAGE ( .BOTH. , #2554 ) ;
#5561=CARTESIAN_POINT ( 'NONE',  ( 498.8117674897343932, 191.8198460455371333, 178.2339398819846110 ) ) ;
#5576=DIRECTION ( 'NONE',  ( 0.000000000000000000, 0.000000000000000000, 1.000000000000000000 ) ) ;
#5582=FILL_AREA_STYLE_COLOUR ( '', #3091 ) ;
#5592=COLOUR_RGB ( '', 0.09019608, 0.27058824, 0.51372549) ;
#5597=EDGE_CURVE ( 'NONE', #16250, #19193, #6255, .T. ) ;
#5598=EDGE_LOOP ( 'NONE', ( #17173, #18479, #4847, #10920 ) ) ;
#5600=UNCERTAINTY_MEASURE_WITH_UNIT (LENGTH_MEASURE( 1.000000000000000082E-05 ), #12950, 'distance_accuracy_value', 'NONE');
#5607=LINE ( 'NONE', #7071, #12027 ) ;
#5610=LINE ( 'NONE', #7072, #4584 ) ;
#5621=( NAMED_UNIT ( * ) SI_UNIT ( $, .STERADIAN. ) SOLID_ANGLE_UNIT ( ) );
#5636=PRESENTATION_STYLE_ASSIGNMENT (( #15118 ) ) ;
#5640=( GEOMETRIC_REPRESENTATION_CONTEXT ( 3 ) GLOBAL_UNCERTAINTY_ASSIGNED_CONTEXT ( ( #2679 ) ) GLOBAL_UNIT_ASSIGNED_CONTEXT ( ( #20149, #18503, #10689 ) ) REPRESENTATION_CONTEXT ( 'NONE', 'WORKASPACE' ) );
#5641=LINE ( 'NONE', #880, #10635 ) ;
#5650=VERTEX_POINT ( 'NONE', #13456 ) ;
#5653=AXIS2_PLACEMENT_3D ( 'NONE', #12131, #1266, #2849 ) ;
#5656=STYLED_ITEM ( 'NONE', ( #19330 ), #8670 ) ;
#5661=LINE ( 'NONE', #11960, #17117 ) ;
#5672=FACE_BOUND ( 'NONE', #11610, .T. ) ;
#5675=ORIENTED_EDGE ( 'NONE', *, *, #17826, .T. ) ;
#5690=ORIENTED_EDGE ( 'NONE', *, *, #17964, .T. ) ;
#5691=DIRECTION ( 'NONE',  ( -1.000000000000000000, 0.000000000000000000, -0.000000000000000000 ) ) ;
#5695=EDGE_CURVE ( 'NONE', #16024, #10866, #3462, .T. ) ;
#5704=ORIENTED_EDGE ( 'NONE', *, *, #4709, .F. ) ;
#5724=ORIENTED_EDGE ( 'NONE', *, *, #3718, .F. ) ;
#5726=ORIENTED_EDGE ( 'NONE', *, *, #5597, .F. ) ;
#5744=DIRECTION ( 'NONE',  ( 0.000000000000000000, 0.000000000000000000, 1.000000000000000000 ) ) ;
#5751=FILL_AREA_STYLE ('',( #19838 ) ) ;
#5756=EDGE_CURVE ( 'NONE', #13105, #16250, #11483, .T. ) ;
#5761=AXIS2_PLACEMENT_3D ( 'NONE', #13387, #17696, #12976 ) ;
#5762=DIRECTION ( 'NONE',  ( 0.000000000000000000, 0.000000000000000000, -1.000000000000000000 ) ) ;
#5776=EDGE_CURVE ( 'NONE', #2425, #6883, #19495, .T. ) ;
#5788=ORIENTED_EDGE ( 'NONE', *, *, #15909, .F. ) ;
#5795=UNCERTAINTY_MEASURE_WITH_UNIT (LENGTH_MEASURE( 1.000000000000000082E-05 ), #17140, 'distance_accuracy_value', 'NONE');
#5810=( GEOMETRIC_REPRESENTATION_CONTEXT ( 3 ) GLOBAL_UNCERTAINTY_ASSIGNED_CONTEXT ( ( #16006 ) ) GLOBAL_UNIT_ASSIGNED_CONTEXT ( ( #18745, #4334, #15372 ) ) REPRESENTATION_CONTEXT ( 'NONE', 'WORKASPACE' ) );
#5814=EDGE_CURVE ( 'NONE', #17668, #12426, #12850, .T. ) ;
#5822=CARTESIAN_POINT ( 'NONE',  ( 503.8334540492693918, 191.8198460455371333, 178.2339398819846110 ) ) ;
#5823=PRESENTATION_STYLE_ASSIGNMENT (( #10750 ) ) ;
#5832=FILL_AREA_STYLE ('',( #2412 ) ) ;
#5841=FILL_AREA_STYLE_COLOUR ( '', #14968 ) ;
#5846=CARTESIAN_POINT ( 'NONE',  ( 503.8334540492693918, 191.8198460455371333, 24.99421986894476078 ) ) ;
#5855=DIRECTION ( 'NONE',  ( 1.000000000000000000, -0.000000000000000000, -0.000000000000000000 ) ) ;
#5879=DIRECTION ( 'NONE',  ( 0.000000000000000000, 0.000000000000000000, -1.000000000000000000 ) ) ;
#5887=SURFACE_STYLE_USAGE ( .BOTH. , #15695 ) ;
#5902=EDGE_CURVE ( 'NONE', #716, #16512, #16751, .T. ) ;
#5905=STYLED_ITEM ( 'NONE', ( #9371 ), #16097 ) ;
#5910=ORIENTED_EDGE ( 'NONE', *, *, #11303, .T. ) ;
#5915=ORIENTED_EDGE ( 'NONE', *, *, #19947, .T. ) ;
#5925=EDGE_LOOP ( 'NONE', ( #4821, #5726 ) ) ;
#5926=ORIENTED_EDGE ( 'NONE', *, *, #3344, .F. ) ;
#5932=PRESENTATION_STYLE_ASSIGNMENT (( #4200 ) ) ;
#5933=SURFACE_SIDE_STYLE ('',( #20023 ) ) ;
#5956=ORIENTED_EDGE ( 'NONE', *, *, #17325, .T. ) ;
#5971=( NAMED_UNIT ( * ) SI_UNIT ( $, .STERADIAN. ) SOLID_ANGLE_UNIT ( ) );
#5981=VERTEX_POINT ( 'NONE', #7855 ) ;
#5982=PRESENTATION_STYLE_ASSIGNMENT (( #5887 ) ) ;
#5985=UNCERTAINTY_MEASURE_WITH_UNIT (LENGTH_MEASURE( 1.000000000000000082E-05 ), #8719, 'distance_accuracy_value', 'NONE');
#5989=SURFACE_STYLE_USAGE ( .BOTH. , #10524 ) ;
#5991=CARTESIAN_POINT ( 'NONE',  ( 458.8334540492693350, 167.8734308960555950, 0.000000000000000000 ) ) ;
#5998=EDGE_LOOP ( 'NONE', ( #19253, #7844, #8778, #14516 ) ) ;
#6005=VECTOR ( 'NONE', #7694, 1000.000000000000000 ) ;
#6007=VERTEX_POINT ( 'NONE', #7957 ) ;
#6024=ORIENTED_EDGE ( 'NONE', *, *, #4640, .F. ) ;
#6039=COLOUR_RGB ( '', 0.40784314, 0.44705882, 0.49803922) ;
#6042=ADVANCED_FACE ( 'NONE', ( #1326 ), #6220, .F. ) ;
#6043=CARTESIAN_POINT ( 'NONE',  ( 406.3334540492693350, 167.8734308960555950, 250.0000000000000000 ) ) ;
#6051=FILL_AREA_STYLE_COLOUR ( '', #1721 ) ;
#6053=DIRECTION ( 'NONE',  ( 0.000000000000000000, -1.000000000000000000, 0.000000000000000000 ) ) ;
#6060=COLOUR_RGB ( '', 0.40784314, 0.44705882, 0.49803922) ;
#6065=ORIENTED_EDGE ( 'NONE', *, *, #13533, .F. ) ;
#6066=FACE_OUTER_BOUND ( 'NONE', #8934, .T. ) ;
#6069=ORIENTED_EDGE ( 'NONE', *, *, #1946, .F. ) ;
#6071=EDGE_CURVE ( 'NONE', #7205, #13831, #2258, .T. ) ;
#6085=STYLED_ITEM ( 'NONE', ( #5932 ), #1009 ) ;
#6086=PRESENTATION_STYLE_ASSIGNMENT (( #17011 ) ) ;
#6087=PRESENTATION_STYLE_ASSIGNMENT (( #20176 ) ) ;
#6103=MECHANICAL_DESIGN_GEOMETRIC_PRESENTATION_REPRESENTATION('',(#8414),#17229);
#6106=CARTESIAN_POINT ( 'NONE',  ( 468.8334540492694487, 214.2156642432025251, 245.0000000000000000 ) ) ;
#6177=DIRECTION ( 'NONE',  ( 0.000000000000000000, -0.000000000000000000, 1.000000000000000000 ) ) ;
#6180=SHAPE_REPRESENTATION ( 'Part11^Assem2', ( #2741 ), #19153 ) ;
#6183=FACE_BOUND ( 'NONE', #2550, .T. ) ;
#6199=ORIENTED_EDGE ( 'NONE', *, *, #3740, .F. ) ;
#6215=VERTEX_POINT ( 'NONE', #10320 ) ;
#6220=CYLINDRICAL_SURFACE ( 'NONE', #12513, 10.00000000000001066 ) ;
#6240=AXIS2_PLACEMENT_3D ( 'NONE', #13529, #17031, #5691 ) ;
#6243=EDGE_CURVE ( 'NONE', #20367, #1837, #10209, .T. ) ;
#6248=SURFACE_STYLE_FILL_AREA ( #7795 ) ;
#6255=CIRCLE ( 'NONE', #12171, 10.00000000000001066 ) ;
#6257=ORIENTED_EDGE ( 'NONE', *, *, #1249, .F. ) ;
#6278=EDGE_CURVE ( 'NONE', #19193, #16250, #290, .T. ) ;
#6289=STYLED_ITEM ( 'NONE', ( #16234 ), #19856 ) ;
#6307=CARTESIAN_POINT ( 'NONE',  ( 486.8117674897343363, 214.2156642432025251, 245.0000000000000000 ) ) ;
#6343=SURFACE_STYLE_FILL_AREA ( #16053 ) ;
#6351=DIRECTION ( 'NONE',  ( 0.000000000000000000, 1.000000000000000000, 0.000000000000000000 ) ) ;
#6356=EDGE_CURVE ( 'NONE', #13581, #9734, #9687, .T. ) ;
#6361=LINE ( 'NONE', #12856, #8669 ) ;
#6372=PLANE ( 'NONE',  #17830 ) ;
#6384=CYLINDRICAL_SURFACE ( 'NONE', #4084, 10.00000000000000888 ) ;
#6390=AXIS2_PLACEMENT_3D ( 'NONE', #3614, #17922, #3911 ) ;
#6391=CARTESIAN_POINT ( 'NONE',  ( 498.8334540492693918, 191.8198460455371333, 225.0057801310552463 ) ) ;
#6408=CARTESIAN_POINT ( 'NONE',  ( 423.8334540492694487, 191.8198460455371333, 168.2339398819845826 ) ) ;
#6418=ADVANCED_FACE ( 'NONE', ( #6609 ), #12900, .F. ) ;
#6424=CIRCLE ( 'NONE', #9040, 10.00000000000000888 ) ;
#6429=ORIENTED_EDGE ( 'NONE', *, *, #2369, .T. ) ;
#6449=VERTEX_POINT ( 'NONE', #8648 ) ;
#6455=DIRECTION ( 'NONE',  ( 0.000000000000000000, 0.000000000000000000, -1.000000000000000000 ) ) ;
#6456=CARTESIAN_POINT ( 'NONE',  ( 498.8334540492693918, 167.8734308960555950, 250.0000000000000000 ) ) ;
#6459=DIRECTION ( 'NONE',  ( 0.000000000000000000, 0.000000000000000000, -1.000000000000000000 ) ) ;
#6489=CARTESIAN_POINT ( 'NONE',  ( 423.8334540492694487, 191.8198460455371333, 81.76606011801540319 ) ) ;
#6493=UNCERTAINTY_MEASURE_WITH_UNIT (LENGTH_MEASURE( 1.000000000000000082E-05 ), #19627, 'distance_accuracy_value', 'NONE');
#6502=CARTESIAN_POINT ( 'NONE',  ( 475.8334540492694487, 214.2156642432025251, 245.0000000000000000 ) ) ;
#6504=EDGE_CURVE ( 'NONE', #6007, #19270, #984, .T. ) ;
#6510=ADVANCED_FACE ( 'NONE', ( #2350 ), #2463, .F. ) ;
#6514=FILL_AREA_STYLE_COLOUR ( '', #4106 ) ;
#6517=ORIENTED_EDGE ( 'NONE', *, *, #17826, .F. ) ;
#6530=ADVANCED_FACE ( 'NONE', ( #1089, #13788, #17294, #15767, #20368 ), #12457, .F. ) ;
#6551=DIRECTION ( 'NONE',  ( 1.000000000000000000, 0.000000000000000000, 0.000000000000000000 ) ) ;
#6561=VERTEX_POINT ( 'NONE', #10909 ) ;
#6575=VERTEX_POINT ( 'NONE', #4314 ) ;
#6578=COLOUR_RGB ( '', 0.31764706, 0.68627451, 0.89019608) ;
#6581=MECHANICAL_DESIGN_GEOMETRIC_PRESENTATION_REPRESENTATION('',(#4922),#9528);
#6586=CARTESIAN_POINT ( 'NONE',  ( 463.8334540492693350, 214.2156642432025251, -87.31255586191144857 ) ) ;
#6592=ADVANCED_FACE ( 'NONE', ( #10805, #4722, #6183, #2859, #12241 ), #15672, .T. ) ;
#6595=SURFACE_STYLE_FILL_AREA ( #1832 ) ;
#6608=( LENGTH_UNIT ( ) NAMED_UNIT ( * ) SI_UNIT ( .MILLI., .METRE. ) );
#6609=FACE_OUTER_BOUND ( 'NONE', #4585, .T. ) ;
#6658=( NAMED_UNIT ( * ) PLANE_ANGLE_UNIT ( ) SI_UNIT ( $, .RADIAN. ) );
#6659=MECHANICAL_DESIGN_GEOMETRIC_PRESENTATION_REPRESENTATION('',(#8941),#11238);
#6668=DIRECTION ( 'NONE',  ( 1.000000000000000000, -0.000000000000000000, -0.000000000000000000 ) ) ;
#6673=CIRCLE ( 'NONE', #18148, 10.00000000000000888 ) ;
#6676=CARTESIAN_POINT ( 'NONE',  ( 423.8334540492694487, 191.8198460455371333, 81.76606011801540319 ) ) ;
#6686=STYLED_ITEM ( 'NONE', ( #13388 ), #8244 ) ;
#6699=CIRCLE ( 'NONE', #7349, 10.00000000000000888 ) ;
#6704=ORIENTED_EDGE ( 'NONE', *, *, #12967, .T. ) ;
#6707=EDGE_LOOP ( 'NONE', ( #7346, #5788 ) ) ;
#6733=MECHANICAL_DESIGN_GEOMETRIC_PRESENTATION_REPRESENTATION('',(#9668),#9343);
#6752=( GEOMETRIC_REPRESENTATION_CONTEXT ( 3 ) GLOBAL_UNCERTAINTY_ASSIGNED_CONTEXT ( ( #11557 ) ) GLOBAL_UNIT_ASSIGNED_CONTEXT ( ( #4182, #15188, #4269 ) ) REPRESENTATION_CONTEXT ( 'NONE', 'WORKASPACE' ) );
#6756=STYLED_ITEM ( 'NONE', ( #9489 ), #15873 ) ;
#6770=AXIS2_PLACEMENT_3D ( 'NONE', #20027, #7687, #4387 ) ;
#6781=CYLINDRICAL_SURFACE ( 'NONE', #2919, 10.00000000000000888 ) ;
#6793=VERTEX_POINT ( 'NONE', #15115 ) ;
#6796=SURFACE_SIDE_STYLE ('',( #2214 ) ) ;
#6799=( NAMED_UNIT ( * ) PLANE_ANGLE_UNIT ( ) SI_UNIT ( $, .RADIAN. ) );
#6802=ORIENTED_EDGE ( 'NONE', *, *, #9833, .T. ) ;
#6837=UNCERTAINTY_MEASURE_WITH_UNIT (LENGTH_MEASURE( 1.000000000000000082E-05 ), #2473, 'distance_accuracy_value', 'NONE');
#6842=UNCERTAINTY_MEASURE_WITH_UNIT (LENGTH_MEASURE( 1.000000000000000082E-05 ), #11983, 'distance_accuracy_value', 'NONE');
#6846=ORIENTED_EDGE ( 'NONE', *, *, #18429, .T. ) ;
#6854=EDGE_LOOP ( 'NONE', ( #1182, #1898, #8696, #2121 ) ) ;
#6862=ORIENTED_EDGE ( 'NONE', *, *, #2310, .T. ) ;
#6869=CARTESIAN_POINT ( 'NONE',  ( 463.8334540492693350, 191.8198460455371333, 81.76606011801540319 ) ) ;
#6873=DIRECTION ( 'NONE',  ( 1.000000000000000000, -0.000000000000000000, -0.000000000000000000 ) ) ;
#6879=CARTESIAN_POINT ( 'NONE',  ( 423.8334540492694487, 191.8198460455371333, 225.0057801310552463 ) ) ;
#6883=VERTEX_POINT ( 'NONE', #13977 ) ;
#6888=ORIENTED_EDGE ( 'NONE', *, *, #14826, .T. ) ;
#6931=FILL_AREA_STYLE_COLOUR ( '', #5431 ) ;
#6947=CYLINDRICAL_SURFACE ( 'NONE', #5301, 10.00000000000000888 ) ;
#6967=VERTEX_POINT ( 'NONE', #2929 ) ;
#6968=LINE ( 'NONE', #460, #268 ) ;
#6974=LINE ( 'NONE', #17578, #14860 ) ;
#6978=( GEOMETRIC_REPRESENTATION_CONTEXT ( 3 ) GLOBAL_UNCERTAINTY_ASSIGNED_CONTEXT ( ( #14324 ) ) GLOBAL_UNIT_ASSIGNED_CONTEXT ( ( #19246, #15978, #17887 ) ) REPRESENTATION_CONTEXT ( 'NONE', 'WORKASPACE' ) );
#6981=ORIENTED_EDGE ( 'NONE', *, *, #15457, .T. ) ;
#6985=( LENGTH_UNIT ( ) NAMED_UNIT ( * ) SI_UNIT ( .MILLI., .METRE. ) );
#6992=DIRECTION ( 'NONE',  ( 1.000000000000000000, -0.000000000000000000, -0.000000000000000000 ) ) ;
#7002=LINE ( 'NONE', #594, #19120 ) ;
#7021=CARTESIAN_POINT ( 'NONE',  ( 458.8334540492693350, 191.8198460455371333, 158.2339398819845826 ) ) ;
#7023=MECHANICAL_DESIGN_GEOMETRIC_PRESENTATION_REPRESENTATION('',(#15905),#7332);
#7044=ORIENTED_EDGE ( 'NONE', *, *, #2369, .F. ) ;
#7050=DIRECTION ( 'NONE',  ( 0.000000000000000000, 0.000000000000000000, 1.000000000000000000 ) ) ;
#7064=CARTESIAN_POINT ( 'NONE',  ( 463.8334540492693350, 191.8198460455371333, 81.76606011801540319 ) ) ;
#7071=CARTESIAN_POINT ( 'NONE',  ( 463.8334540492693918, 167.8734308960555950, 250.0000000000000000 ) ) ;
#7072=CARTESIAN_POINT ( 'NONE',  ( 423.8334540492694487, 191.8198460455371333, 71.76606011801538898 ) ) ;
#7089=ORIENTED_EDGE ( 'NONE', *, *, #15974, .F. ) ;
#7106=CARTESIAN_POINT ( 'NONE',  ( 458.8334540492693350, 0.000000000000000000, 0.000000000000000000 ) ) ;
#7108=UNCERTAINTY_MEASURE_WITH_UNIT (LENGTH_MEASURE( 1.000000000000000082E-05 ), #13008, 'distance_accuracy_value', 'NONE');
#7111=ORIENTED_EDGE ( 'NONE', *, *, #10734, .F. ) ;
#7121=CARTESIAN_POINT ( 'NONE',  ( 463.8334540492693350, 214.2156642432025251, 250.0000000000000000 ) ) ;
#7134=DIRECTION ( 'NONE',  ( -1.000000000000000000, 0.000000000000000000, -0.000000000000000000 ) ) ;
#7141=ORIENTED_EDGE ( 'NONE', *, *, #7859, .F. ) ;
#7144=CARTESIAN_POINT ( 'NONE',  ( 0.000000000000000000, 0.000000000000000000, 0.000000000000000000 ) ) ;
#7160=( LENGTH_UNIT ( ) NAMED_UNIT ( * ) SI_UNIT ( .MILLI., .METRE. ) );
#7176=FACE_OUTER_BOUND ( 'NONE', #15559, .T. ) ;
#7197=LINE ( 'NONE', #19633, #19488 ) ;
#7199=SURFACE_STYLE_FILL_AREA ( #5751 ) ;
#7202=AXIS2_PLACEMENT_3D ( 'NONE', #15651, #3162, #9442 ) ;
#7205=VERTEX_POINT ( 'NONE', #9058 ) ;
#7207=PRODUCT_DEFINITION_CONTEXT ( 'detailed design', #18669, 'design' ) ;
#7212=DIRECTION ( 'NONE',  ( 0.000000000000000000, 0.000000000000000000, -1.000000000000000000 ) ) ;
#7224=FACE_OUTER_BOUND ( 'NONE', #6854, .T. ) ;
#7225=AXIS2_PLACEMENT_3D ( 'NONE', #18443, #17320, #13918 ) ;
#7229=ORIENTED_EDGE ( 'NONE', *, *, #2310, .F. ) ;
#7233=SURFACE_STYLE_FILL_AREA ( #717 ) ;
#7249=PLANE ( 'NONE',  #6240 ) ;
#7253=( GEOMETRIC_REPRESENTATION_CONTEXT ( 3 ) GLOBAL_UNCERTAINTY_ASSIGNED_CONTEXT ( ( #5453 ) ) GLOBAL_UNIT_ASSIGNED_CONTEXT ( ( #20315, #9591, #15911 ) ) REPRESENTATION_CONTEXT ( 'NONE', 'WORKASPACE' ) );
#7254=VERTEX_POINT ( 'NONE', #12916 ) ;
#7259=UNCERTAINTY_MEASURE_WITH_UNIT (LENGTH_MEASURE( 1.000000000000000082E-05 ), #6985, 'distance_accuracy_value', 'NONE');
#7262=( LENGTH_UNIT ( ) NAMED_UNIT ( * ) SI_UNIT ( .MILLI., .METRE. ) );
#7275=CARTESIAN_POINT ( 'NONE',  ( 468.8334540492694487, 134.2156642432025251, 245.0000000000000000 ) ) ;
#7278=( GEOMETRIC_REPRESENTATION_CONTEXT ( 3 ) GLOBAL_UNCERTAINTY_ASSIGNED_CONTEXT ( ( #423 ) ) GLOBAL_UNIT_ASSIGNED_CONTEXT ( ( #18425, #11861, #5971 ) ) REPRESENTATION_CONTEXT ( 'NONE', 'WORKASPACE' ) );
#7281=ORIENTED_EDGE ( 'NONE', *, *, #15457, .F. ) ;
#7310=MECHANICAL_DESIGN_GEOMETRIC_PRESENTATION_REPRESENTATION('',(#5656),#8605);
#7317=( NAMED_UNIT ( * ) SI_UNIT ( $, .STERADIAN. ) SOLID_ANGLE_UNIT ( ) );
#7318=AXIS2_PLACEMENT_3D ( 'NONE', #17143, #15827, #1661 ) ;
#7332=( GEOMETRIC_REPRESENTATION_CONTEXT ( 3 ) GLOBAL_UNCERTAINTY_ASSIGNED_CONTEXT ( ( #13615 ) ) GLOBAL_UNIT_ASSIGNED_CONTEXT ( ( #2939, #3040, #9336 ) ) REPRESENTATION_CONTEXT ( 'NONE', 'WORKASPACE' ) );
#7340=LINE ( 'NONE', #14977, #10998 ) ;
#7346=ORIENTED_EDGE ( 'NONE', *, *, #2069, .F. ) ;
#7349=AXIS2_PLACEMENT_3D ( 'NONE', #11566, #11465, #12924 ) ;
#7351=EDGE_CURVE ( 'NONE', #7872, #20367, #7952, .T. ) ;
#7372=MECHANICAL_DESIGN_GEOMETRIC_PRESENTATION_REPRESENTATION('',(#6085),#9331);
#7381=( GEOMETRIC_REPRESENTATION_CONTEXT ( 3 ) GLOBAL_UNCERTAINTY_ASSIGNED_CONTEXT ( ( #11773 ) ) GLOBAL_UNIT_ASSIGNED_CONTEXT ( ( #17007, #12461, #7613 ) ) REPRESENTATION_CONTEXT ( 'NONE', 'WORKASPACE' ) );
#7387=ORIENTED_EDGE ( 'NONE', *, *, #18049, .T. ) ;
#7397=AXIS2_PLACEMENT_3D ( 'NONE', #16507, #5474, #7134 ) ;
#7422=FACE_OUTER_BOUND ( 'NONE', #391, .T. ) ;
#7424=( LENGTH_UNIT ( ) NAMED_UNIT ( * ) SI_UNIT ( .MILLI., .METRE. ) );
#7433=DIRECTION ( 'NONE',  ( 1.000000000000000000, -0.000000000000000000, -0.000000000000000000 ) ) ;
#7434=CYLINDRICAL_SURFACE ( 'NONE', #15165, 10.00000000000000888 ) ;
#7438=ORIENTED_EDGE ( 'NONE', *, *, #15437, .T. ) ;
#7443=DIRECTION ( 'NONE',  ( 1.000000000000000000, 0.000000000000000000, 0.000000000000000000 ) ) ;
#7444=MECHANICAL_DESIGN_GEOMETRIC_PRESENTATION_REPRESENTATION('',(#16015),#2484);
#7449=FACE_OUTER_BOUND ( 'NONE', #12090, .T. ) ;
#7482=EDGE_LOOP ( 'NONE', ( #15356, #38 ) ) ;
#7492=VERTEX_POINT ( 'NONE', #19580 ) ;
#7495=DIRECTION ( 'NONE',  ( 1.000000000000000000, 0.000000000000000000, 0.000000000000000000 ) ) ;
#7496=( NAMED_UNIT ( * ) PLANE_ANGLE_UNIT ( ) SI_UNIT ( $, .RADIAN. ) );
#7517=DIRECTION ( 'NONE',  ( -1.000000000000000000, 0.000000000000000000, -0.000000000000000000 ) ) ;
#7518=CARTESIAN_POINT ( 'NONE',  ( 503.8334540492693918, 191.8198460455371333, 81.76606011801540319 ) ) ;
#7522=( NAMED_UNIT ( * ) SI_UNIT ( $, .STERADIAN. ) SOLID_ANGLE_UNIT ( ) );
#7524=PLANE ( 'NONE',  #994 ) ;
#7528=ORIENTED_EDGE ( 'NONE', *, *, #12663, .T. ) ;
#7537=SURFACE_STYLE_USAGE ( .BOTH. , #2577 ) ;
#7541=DIRECTION ( 'NONE',  ( 0.000000000000000000, 1.000000000000000000, 0.000000000000000000 ) ) ;
#7542=LINE ( 'NONE', #5991, #19481 ) ;
#7551=MECHANICAL_DESIGN_GEOMETRIC_PRESENTATION_REPRESENTATION('',(#13842),#3619);
#7553=VECTOR ( 'NONE', #19402, 1000.000000000000000 ) ;
#7568=FILL_AREA_STYLE ('',( #1236 ) ) ;
#7579=( NAMED_UNIT ( * ) PLANE_ANGLE_UNIT ( ) SI_UNIT ( $, .RADIAN. ) );
#7588=EDGE_CURVE ( 'NONE', #11175, #3837, #16511, .T. ) ;
#7591=( LENGTH_UNIT ( ) NAMED_UNIT ( * ) SI_UNIT ( .MILLI., .METRE. ) );
#7606=DIRECTION ( 'NONE',  ( 0.000000000000000000, 1.000000000000000000, 0.000000000000000000 ) ) ;
#7609=( GEOMETRIC_REPRESENTATION_CONTEXT ( 3 ) GLOBAL_UNCERTAINTY_ASSIGNED_CONTEXT ( ( #10728 ) ) GLOBAL_UNIT_ASSIGNED_CONTEXT ( ( #4843, #1401, #11023 ) ) REPRESENTATION_CONTEXT ( 'NONE', 'WORKASPACE' ) );
#7610=DIRECTION ( 'NONE',  ( 0.000000000000000000, 0.000000000000000000, 1.000000000000000000 ) ) ;
#7613=( NAMED_UNIT ( * ) SI_UNIT ( $, .STERADIAN. ) SOLID_ANGLE_UNIT ( ) );
#7618=SURFACE_STYLE_FILL_AREA ( #1292 ) ;
#7620=EDGE_LOOP ( 'NONE', ( #8694, #3814, #6704, #13219 ) ) ;
#7648=CIRCLE ( 'NONE', #8952, 10.00000000000000888 ) ;
#7655=FILL_AREA_STYLE ('',( #7767 ) ) ;
#7658=DIRECTION ( 'NONE',  ( 1.000000000000000000, 0.000000000000000000, 0.000000000000000000 ) ) ;
#7670=VECTOR ( 'NONE', #19634, 1000.000000000000000 ) ;
#7681=CARTESIAN_POINT ( 'NONE',  ( 498.8117674897343932, 191.8198460455371333, 168.2339398819845826 ) ) ;
#7687=DIRECTION ( 'NONE',  ( 1.000000000000000000, 0.000000000000000000, 0.000000000000000000 ) ) ;
#7688=DIRECTION ( 'NONE',  ( 1.000000000000000000, 0.000000000000000000, -0.000000000000000000 ) ) ;
#7694=DIRECTION ( 'NONE',  ( 1.000000000000000000, -0.000000000000000000, -0.000000000000000000 ) ) ;
#7696=( NAMED_UNIT ( * ) PLANE_ANGLE_UNIT ( ) SI_UNIT ( $, .RADIAN. ) );
#7703=COLOUR_RGB ( '', 0.40784314, 0.44705882, 0.49803922) ;
#7714=ORIENTED_EDGE ( 'NONE', *, *, #1797, .F. ) ;
#7717=FILL_AREA_STYLE ('',( #1391 ) ) ;
#7721=CARTESIAN_POINT ( 'NONE',  ( 498.8117674897343932, 191.8198460455371333, 71.76606011801538898 ) ) ;
#7734=CARTESIAN_POINT ( 'NONE',  ( 423.8334540492694487, 191.8198460455371333, 158.2339398819845826 ) ) ;
#7738=CARTESIAN_POINT ( 'NONE',  ( 458.8334540492693350, 0.000000000000000000, 0.000000000000000000 ) ) ;
#7742=ADVANCED_FACE ( 'NONE', ( #14217 ), #12477, .F. ) ;
#7748=VECTOR ( 'NONE', #20260, 1000.000000000000000 ) ;
#7750=CARTESIAN_POINT ( 'NONE',  ( 423.8334540492694487, 191.8198460455371333, 24.99421986894476078 ) ) ;
#7762=ORIENTED_EDGE ( 'NONE', *, *, #385, .T. ) ;
#7767=FILL_AREA_STYLE_COLOUR ( '', #19723 ) ;
#7768=ORIENTED_EDGE ( 'NONE', *, *, #9990, .F. ) ;
#7771=( GEOMETRIC_REPRESENTATION_CONTEXT ( 3 ) GLOBAL_UNCERTAINTY_ASSIGNED_CONTEXT ( ( #2060 ) ) GLOBAL_UNIT_ASSIGNED_CONTEXT ( ( #15267, #2681, #18656 ) ) REPRESENTATION_CONTEXT ( 'NONE', 'WORKASPACE' ) );
#7775=CARTESIAN_POINT ( 'NONE',  ( 498.8334540492693918, 191.8198460455371333, 158.2339398819845826 ) ) ;
#7793=DIRECTION ( 'NONE',  ( 0.000000000000000000, 0.000000000000000000, -1.000000000000000000 ) ) ;
#7795=FILL_AREA_STYLE ('',( #1475 ) ) ;
#7798=CYLINDRICAL_SURFACE ( 'NONE', #10492, 10.00000000000000888 ) ;
#7806=CARTESIAN_POINT ( 'NONE',  ( 498.8117674897343932, 214.2156642432025251, 0.000000000000000000 ) ) ;
#7811=EDGE_CURVE ( 'NONE', #13581, #12734, #19356, .T. ) ;
#7818=( NAMED_UNIT ( * ) SI_UNIT ( $, .STERADIAN. ) SOLID_ANGLE_UNIT ( ) );
#7844=ORIENTED_EDGE ( 'NONE', *, *, #2414, .T. ) ;
#7849=EDGE_LOOP ( 'NONE', ( #3739, #15198 ) ) ;
#7851=ADVANCED_FACE ( 'NONE', ( #18108, #19276, #2348, #11753, #604 ), #11441, .F. ) ;
#7855=CARTESIAN_POINT ( 'NONE',  ( 503.8334540492693918, 191.8198460455371333, 215.0057801310552179 ) ) ;
#7859=EDGE_CURVE ( 'NONE', #13299, #10437, #9889, .T. ) ;
#7865=LINE ( 'NONE', #17136, #10360 ) ;
#7872=VERTEX_POINT ( 'NONE', #511 ) ;
#7874=VERTEX_POINT ( 'NONE', #9993 ) ;
#7885=VECTOR ( 'NONE', #5855, 1000.000000000000000 ) ;
#7887=DIRECTION ( 'NONE',  ( -1.000000000000000000, 0.000000000000000000, 0.000000000000000000 ) ) ;
#7889=SURFACE_STYLE_FILL_AREA ( #3253 ) ;
#7895=SURFACE_STYLE_USAGE ( .BOTH. , #18800 ) ;
#7908=VECTOR ( 'NONE', #8177, 1000.000000000000000 ) ;
#7924=MECHANICAL_DESIGN_GEOMETRIC_PRESENTATION_REPRESENTATION('',(#6289),#13208);
#7928=EDGE_LOOP ( 'NONE', ( #8195, #11055 ) ) ;
#7929=UNCERTAINTY_MEASURE_WITH_UNIT (LENGTH_MEASURE( 1.000000000000000082E-05 ), #12701, 'distance_accuracy_value', 'NONE');
#7952=LINE ( 'NONE', #4659, #19754 ) ;
#7957=CARTESIAN_POINT ( 'NONE',  ( 468.8334540492694487, 214.2156642432025251, 250.0000000000000000 ) ) ;
#7960=CARTESIAN_POINT ( 'NONE',  ( 463.8334540492693350, 191.8198460455371333, 158.2339398819845826 ) ) ;
#7973=CIRCLE ( 'NONE', #9954, 10.00000000000000888 ) ;
#7977=EDGE_LOOP ( 'NONE', ( #7089, #4431, #15638, #13671 ) ) ;
#7978=CARTESIAN_POINT ( 'NONE',  ( 493.8117674897343363, 214.2156642432025251, 245.0000000000000000 ) ) ;
#7982=STYLED_ITEM ( 'NONE', ( #12390 ), #11689 ) ;
#7987=ADVANCED_FACE ( 'NONE', ( #7422 ), #2657, .F. ) ;
#8000=SURFACE_STYLE_USAGE ( .BOTH. , #15654 ) ;
#8006=ORIENTED_EDGE ( 'NONE', *, *, #18614, .F. ) ;
#8009=AXIS2_PLACEMENT_3D ( 'NONE', #1008, #11877, #8972 ) ;
#8012=DIRECTION ( 'NONE',  ( -1.000000000000000000, 0.000000000000000000, -0.000000000000000000 ) ) ;
#8024=AXIS2_PLACEMENT_3D ( 'NONE', #17898, #3800, #492 ) ;
#8032=VERTEX_POINT ( 'NONE', #18724 ) ;
#8058=AXIS2_PLACEMENT_3D ( 'NONE', #13, #19056, #3210 ) ;
#8065=EDGE_LOOP ( 'NONE', ( #17758, #4777, #13824, #16303 ) ) ;
#8066=STYLED_ITEM ( 'NONE', ( #5636 ), #10842 ) ;
#8072=VERTEX_POINT ( 'NONE', #15670 ) ;
#8075=CARTESIAN_POINT ( 'NONE',  ( 463.8334540492693350, 191.8198460455371333, 71.76606011801538898 ) ) ;
#8077=CARTESIAN_POINT ( 'NONE',  ( 458.8334540492693350, 191.8198460455371333, 235.0057801310552463 ) ) ;
#8081=DIRECTION ( 'NONE',  ( 0.000000000000000000, 0.000000000000000000, -1.000000000000000000 ) ) ;
#8091=EDGE_CURVE ( 'NONE', #12278, #417, #4522, .T. ) ;
#8092=VERTEX_POINT ( 'NONE', #15556 ) ;
#8109=PRODUCT_DEFINITION ( 'UNKNOWN', '', #15243, #7207 ) ;
#8110=ORIENTED_EDGE ( 'NONE', *, *, #10898, .T. ) ;
#8125=SURFACE_STYLE_USAGE ( .BOTH. , #6796 ) ;
#8143=FACE_OUTER_BOUND ( 'NONE', #9102, .T. ) ;
#8150=LINE ( 'NONE', #12787, #13974 ) ;
#8152=ORIENTED_EDGE ( 'NONE', *, *, #17321, .F. ) ;
#8161=( LENGTH_UNIT ( ) NAMED_UNIT ( * ) SI_UNIT ( .MILLI., .METRE. ) );
#8168=VECTOR ( 'NONE', #1457, 1000.000000000000000 ) ;
#8177=DIRECTION ( 'NONE',  ( 1.000000000000000000, 0.000000000000000000, 0.000000000000000000 ) ) ;
#8181=SURFACE_STYLE_FILL_AREA ( #9719 ) ;
#8183=DIRECTION ( 'NONE',  ( -0.000000000000000000, 1.000000000000000000, -0.000000000000000000 ) ) ;
#8186=DIRECTION ( 'NONE',  ( 1.000000000000000000, 0.000000000000000000, 0.000000000000000000 ) ) ;
#8187=VECTOR ( 'NONE', #16165, 1000.000000000000000 ) ;
#8195=ORIENTED_EDGE ( 'NONE', *, *, #19315, .T. ) ;
#8198=FACE_BOUND ( 'NONE', #18565, .T. ) ;
#8204=CARTESIAN_POINT ( 'NONE',  ( 503.8334540492693918, 167.8734308960555950, 0.000000000000000000 ) ) ;
#8209=CARTESIAN_POINT ( 'NONE',  ( 493.8117674897343363, 214.2156642432025251, 250.0000000000000000 ) ) ;
#8218=CARTESIAN_POINT ( 'NONE',  ( 423.8334540492694487, 191.8198460455371333, 168.2339398819845826 ) ) ;
#8234=DIRECTION ( 'NONE',  ( 1.000000000000000000, 0.000000000000000000, 0.000000000000000000 ) ) ;
#8243=VERTEX_POINT ( 'NONE', #16976 ) ;
#8244=ADVANCED_FACE ( 'NONE', ( #4094 ), #15213, .F. ) ;
#8245=LINE ( 'NONE', #11218, #11336 ) ;
#8248=DIRECTION ( 'NONE',  ( 0.000000000000000000, 1.000000000000000000, 0.000000000000000000 ) ) ;
#8258=MECHANICAL_DESIGN_GEOMETRIC_PRESENTATION_REPRESENTATION('',(#11548),#14840);
#8281=STYLED_ITEM ( 'NONE', ( #18005 ), #17398 ) ;
#8310=DIRECTION ( 'NONE',  ( 1.000000000000000000, 0.000000000000000000, -0.000000000000000000 ) ) ;
#8312=SURFACE_SIDE_STYLE ('',( #17575 ) ) ;
#8314=( NAMED_UNIT ( * ) SI_UNIT ( $, .STERADIAN. ) SOLID_ANGLE_UNIT ( ) );
#8318=CARTESIAN_POINT ( 'NONE',  ( 468.8334540492694487, 134.2156642432025251, 250.0000000000000000 ) ) ;
#8331=VERTEX_POINT ( 'NONE', #6456 ) ;
#8341=DIRECTION ( 'NONE',  ( 0.000000000000000000, 0.000000000000000000, -1.000000000000000000 ) ) ;
#8348=EDGE_LOOP ( 'NONE', ( #19970, #13632, #3853, #10464 ) ) ;
#8351=LINE ( 'NONE', #19352, #17316 ) ;
#8361=MECHANICAL_DESIGN_GEOMETRIC_PRESENTATION_REPRESENTATION('',(#4407),#10986);
#8375=VERTEX_POINT ( 'NONE', #11588 ) ;
#8381=CARTESIAN_POINT ( 'NONE',  ( 458.8334540492693350, 191.8198460455371333, 34.99421986894476788 ) ) ;
#8385=( GEOMETRIC_REPRESENTATION_CONTEXT ( 3 ) GLOBAL_UNCERTAINTY_ASSIGNED_CONTEXT ( ( #6842 ) ) GLOBAL_UNIT_ASSIGNED_CONTEXT ( ( #11983, #8976, #1214 ) ) REPRESENTATION_CONTEXT ( 'NONE', 'WORKASPACE' ) );
#8398=CIRCLE ( 'NONE', #5761, 10.00000000000000888 ) ;
#8400=EDGE_CURVE ( 'NONE', #417, #8375, #3564, .T. ) ;
#8405=FILL_AREA_STYLE ('',( #9938 ) ) ;
#8406=CIRCLE ( 'NONE', #15317, 10.00000000000000888 ) ;
#8412=AXIS2_PLACEMENT_3D ( 'NONE', #18237, #2252, #4149 ) ;
#8414=STYLED_ITEM ( 'NONE', ( #20340 ), #1151 ) ;
#8422=FACE_OUTER_BOUND ( 'NONE', #13492, .T. ) ;
#8428=CIRCLE ( 'NONE', #8746, 10.00000000000000888 ) ;
#8433=CYLINDRICAL_SURFACE ( 'NONE', #5002, 10.00000000000000888 ) ;
#8438=ORIENTED_EDGE ( 'NONE', *, *, #18614, .T. ) ;
#8449=VERTEX_POINT ( 'NONE', #17675 ) ;
#8450=EDGE_CURVE ( 'NONE', #15201, #3980, #10623, .T. ) ;
#8455=ORIENTED_EDGE ( 'NONE', *, *, #4695, .F. ) ;
#8459=FILL_AREA_STYLE ('',( #8646 ) ) ;
#8460=DIRECTION ( 'NONE',  ( -0.000000000000000000, -0.000000000000000000, 1.000000000000000000 ) ) ;
#8467=UNCERTAINTY_MEASURE_WITH_UNIT (LENGTH_MEASURE( 1.000000000000000082E-05 ), #15028, 'distance_accuracy_value', 'NONE');
#8501=ADVANCED_FACE ( 'NONE', ( #11901 ), #746, .T. ) ;
#8504=FILL_AREA_STYLE ('',( #2105 ) ) ;
#8510=ORIENTED_EDGE ( 'NONE', *, *, #18804, .F. ) ;
#8532=COLOUR_RGB ( '', 0.31764706, 0.68627451, 0.89019608) ;
#8538=CARTESIAN_POINT ( 'NONE',  ( 463.8334540492693350, 191.8198460455371333, 24.99421986894476078 ) ) ;
#8540=SURFACE_STYLE_USAGE ( .BOTH. , #5360 ) ;
#8574=CIRCLE ( 'NONE', #19420, 10.00000000000000888 ) ;
#8579=ORIENTED_EDGE ( 'NONE', *, *, #10249, .T. ) ;
#8582=MECHANICAL_DESIGN_GEOMETRIC_PRESENTATION_REPRESENTATION('',(#8281),#17814);
#8590=FILL_AREA_STYLE ('',( #16363 ) ) ;
#8594=CARTESIAN_POINT ( 'NONE',  ( 458.8334540492693350, 191.8198460455371333, 24.99421986894476078 ) ) ;
#8599=EDGE_LOOP ( 'NONE', ( #9169, #6069, #17663, #10657 ) ) ;
#8605=( GEOMETRIC_REPRESENTATION_CONTEXT ( 3 ) GLOBAL_UNCERTAINTY_ASSIGNED_CONTEXT ( ( #3400 ) ) GLOBAL_UNIT_ASSIGNED_CONTEXT ( ( #11505, #9859, #16274 ) ) REPRESENTATION_CONTEXT ( 'NONE', 'WORKASPACE' ) );
#8607=ADVANCED_FACE ( 'NONE', ( #17287 ), #6372, .F. ) ;
#8611=ADVANCED_FACE ( 'NONE', ( #6066 ), #17477, .F. ) ;
#8621=CARTESIAN_POINT ( 'NONE',  ( 463.8334540492693350, 214.2156642432025251, 0.000000000000000000 ) ) ;
#8625=LINE ( 'NONE', #7106, #7670 ) ;
#8635=COLOUR_RGB ( '', 0.31764706, 0.68627451, 0.89019608) ;
#8642=DIRECTION ( 'NONE',  ( 1.000000000000000000, 1.197852309262419498E-15, -0.000000000000000000 ) ) ;
#8646=FILL_AREA_STYLE_COLOUR ( '', #7703 ) ;
#8648=CARTESIAN_POINT ( 'NONE',  ( 458.8334540492693350, 242.8734308960556234, 250.0000000000000000 ) ) ;
#8657=EDGE_CURVE ( 'NONE', #6561, #13659, #16381, .T. ) ;
#8658=CARTESIAN_POINT ( 'NONE',  ( 463.8334540492693918, 167.8734308960555950, 0.000000000000000000 ) ) ;
#8667=ORIENTED_EDGE ( 'NONE', *, *, #14645, .T. ) ;
#8669=VECTOR ( 'NONE', #19113, 1000.000000000000000 ) ;
#8670=ADVANCED_FACE ( 'NONE', ( #1903 ), #8433, .F. ) ;
#8671=VERTEX_POINT ( 'NONE', #579 ) ;
#8676=DIRECTION ( 'NONE',  ( 1.000000000000000000, -0.000000000000000000, -0.000000000000000000 ) ) ;
#8690=DIRECTION ( 'NONE',  ( 0.000000000000000000, 1.000000000000000000, 0.000000000000000000 ) ) ;
#8694=ORIENTED_EDGE ( 'NONE', *, *, #18049, .F. ) ;
#8696=ORIENTED_EDGE ( 'NONE', *, *, #13338, .T. ) ;
#8702=STYLED_ITEM ( 'NONE', ( #5823 ), #15140 ) ;
#8719=( LENGTH_UNIT ( ) NAMED_UNIT ( * ) SI_UNIT ( .MILLI., .METRE. ) );
#8721=ORIENTED_EDGE ( 'NONE', *, *, #6504, .F. ) ;
#8732=ORIENTED_EDGE ( 'NONE', *, *, #12783, .F. ) ;
#8746=AXIS2_PLACEMENT_3D ( 'NONE', #10643, #4565, #15720 ) ;
#8751=ORIENTED_EDGE ( 'NONE', *, *, #1044, .F. ) ;
#8768=DIRECTION ( 'NONE',  ( 0.000000000000000000, 0.000000000000000000, -1.000000000000000000 ) ) ;
#8778=ORIENTED_EDGE ( 'NONE', *, *, #18180, .T. ) ;
#8807=SURFACE_STYLE_FILL_AREA ( #2514 ) ;
#8812=VECTOR ( 'NONE', #9800, 1000.000000000000000 ) ;
#8818=SHAPE_DEFINITION_REPRESENTATION ( #12386, #6180 ) ;
#8848=VERTEX_POINT ( 'NONE', #19820 ) ;
#8858=FILL_AREA_STYLE ('',( #2767 ) ) ;
#8860=CARTESIAN_POINT ( 'NONE',  ( 458.8334540492693350, 191.8198460455371333, 81.76606011801540319 ) ) ;
#8872=COLOUR_RGB ( '', 0.66274510, 0.83137255, 0.94901961) ;
#8873=CARTESIAN_POINT ( 'NONE',  ( 463.8334540492693350, 191.8198460455371333, 81.76606011801540319 ) ) ;
#8895=UNCERTAINTY_MEASURE_WITH_UNIT (LENGTH_MEASURE( 1.000000000000000082E-05 ), #18791, 'distance_accuracy_value', 'NONE');
#8899=SURFACE_STYLE_FILL_AREA ( #16844 ) ;
#8926=LINE ( 'NONE', #15221, #17381 ) ;
#8931=SURFACE_SIDE_STYLE ('',( #18202 ) ) ;
#8934=EDGE_LOOP ( 'NONE', ( #67, #13777, #128, #5724 ) ) ;
#8941=STYLED_ITEM ( 'NONE', ( #3054 ), #8607 ) ;
#8952=AXIS2_PLACEMENT_3D ( 'NONE', #6391, #2689, #14103 ) ;
#8964=FILL_AREA_STYLE ('',( #19981 ) ) ;
#8972=DIRECTION ( 'NONE',  ( 0.000000000000000000, 0.000000000000000000, -1.000000000000000000 ) ) ;
#8976=( NAMED_UNIT ( * ) PLANE_ANGLE_UNIT ( ) SI_UNIT ( $, .RADIAN. ) );
#8988=ORIENTED_EDGE ( 'NONE', *, *, #15713, .T. ) ;
#8991=EDGE_LOOP ( 'NONE', ( #18289, #10202, #18602, #1816 ) ) ;
#8995=ORIENTED_EDGE ( 'NONE', *, *, #3831, .F. ) ;
#8999=( GEOMETRIC_REPRESENTATION_CONTEXT ( 3 ) GLOBAL_UNCERTAINTY_ASSIGNED_CONTEXT ( ( #13634 ) ) GLOBAL_UNIT_ASSIGNED_CONTEXT ( ( #14941, #804, #14523 ) ) REPRESENTATION_CONTEXT ( 'NONE', 'WORKASPACE' ) );
#9012=ORIENTED_EDGE ( 'NONE', *, *, #16204, .T. ) ;
#9019=COLOUR_RGB ( '', 0.40784314, 0.44705882, 0.49803922) ;
#9032=ADVANCED_FACE ( 'NONE', ( #43 ), #1566, .F. ) ;
#9040=AXIS2_PLACEMENT_3D ( 'NONE', #2157, #13420, #18119 ) ;
#9058=CARTESIAN_POINT ( 'NONE',  ( 463.8334540492693350, 214.2156642432025251, 0.000000000000000000 ) ) ;
#9062=SURFACE_STYLE_USAGE ( .BOTH. , #17183 ) ;
#9071=FACE_OUTER_BOUND ( 'NONE', #8599, .T. ) ;
#9083=COLOUR_RGB ( '', 0.66274510, 0.83137255, 0.94901961) ;
#9085=UNCERTAINTY_MEASURE_WITH_UNIT (LENGTH_MEASURE( 1.000000000000000082E-05 ), #5198, 'distance_accuracy_value', 'NONE');
#9100=CIRCLE ( 'NONE', #4491, 10.00000000000000888 ) ;
#9102=EDGE_LOOP ( 'NONE', ( #7111, #17284, #676, #17513 ) ) ;
#9118=SURFACE_STYLE_FILL_AREA ( #5832 ) ;
#9128=SURFACE_SIDE_STYLE ('',( #20022 ) ) ;
#9140=CARTESIAN_POINT ( 'NONE',  ( 498.8117674897343932, 191.8198460455371333, 158.2339398819845826 ) ) ;
#9155=( LENGTH_UNIT ( ) NAMED_UNIT ( * ) SI_UNIT ( .MILLI., .METRE. ) );
#9169=ORIENTED_EDGE ( 'NONE', *, *, #1713, .F. ) ;
#9171=( LENGTH_UNIT ( ) NAMED_UNIT ( * ) SI_UNIT ( .MILLI., .METRE. ) );
#9173=DIRECTION ( 'NONE',  ( 1.000000000000000000, 0.000000000000000000, -0.000000000000000000 ) ) ;
#9218=STYLED_ITEM ( 'NONE', ( #815 ), #16547 ) ;
#9220=FACE_OUTER_BOUND ( 'NONE', #14821, .T. ) ;
#9221=COLOUR_RGB ( '', 0.66274510, 0.83137255, 0.94901961) ;
#9227=DIRECTION ( 'NONE',  ( 0.000000000000000000, 1.000000000000000000, 0.000000000000000000 ) ) ;
#9237=EDGE_CURVE ( 'NONE', #20154, #8032, #10407, .T. ) ;
#9249=AXIS2_PLACEMENT_3D ( 'NONE', #2336, #2019, #8341 ) ;
#9253=SURFACE_SIDE_STYLE ('',( #1602 ) ) ;
#9261=ADVANCED_FACE ( 'NONE', ( #8198, #17764, #5409, #14470, #346 ), #11694, .F. ) ;
#9266=ORIENTED_EDGE ( 'NONE', *, *, #13907, .F. ) ;
#9272=CARTESIAN_POINT ( 'NONE',  ( 0.000000000000000000, 0.000000000000000000, 250.0000000000000000 ) ) ;
#9276=EDGE_LOOP ( 'NONE', ( #14063, #14423 ) ) ;
#9281=CYLINDRICAL_SURFACE ( 'NONE', #16180, 10.00000000000001066 ) ;
#9282=DIRECTION ( 'NONE',  ( -1.000000000000000000, -0.000000000000000000, -0.000000000000000000 ) ) ;
#9283=ORIENTED_EDGE ( 'NONE', *, *, #12347, .F. ) ;
#9317=CARTESIAN_POINT ( 'NONE',  ( 0.000000000000000000, 0.000000000000000000, 245.0000000000000000 ) ) ;
#9326=CARTESIAN_POINT ( 'NONE',  ( 423.8334540492694487, 191.8198460455371333, 24.99421986894476078 ) ) ;
#9331=( GEOMETRIC_REPRESENTATION_CONTEXT ( 3 ) GLOBAL_UNCERTAINTY_ASSIGNED_CONTEXT ( ( #19795 ) ) GLOBAL_UNIT_ASSIGNED_CONTEXT ( ( #15422, #7579, #13863 ) ) REPRESENTATION_CONTEXT ( 'NONE', 'WORKASPACE' ) );
#9332=DIRECTION ( 'NONE',  ( 1.000000000000000000, 0.000000000000000000, 0.000000000000000000 ) ) ;
#9333=AXIS2_PLACEMENT_3D ( 'NONE', #9272, #4336, #18341 ) ;
#9336=( NAMED_UNIT ( * ) SI_UNIT ( $, .STERADIAN. ) SOLID_ANGLE_UNIT ( ) );
#9343=( GEOMETRIC_REPRESENTATION_CONTEXT ( 3 ) GLOBAL_UNCERTAINTY_ASSIGNED_CONTEXT ( ( #4173 ) ) GLOBAL_UNIT_ASSIGNED_CONTEXT ( ( #17002, #10491, #18415 ) ) REPRESENTATION_CONTEXT ( 'NONE', 'WORKASPACE' ) );
#9344=( GEOMETRIC_REPRESENTATION_CONTEXT ( 3 ) GLOBAL_UNCERTAINTY_ASSIGNED_CONTEXT ( ( #11768 ) ) GLOBAL_UNIT_ASSIGNED_CONTEXT ( ( #7591, #1487, #10889 ) ) REPRESENTATION_CONTEXT ( 'NONE', 'WORKASPACE' ) );
#9351=DIRECTION ( 'NONE',  ( 0.000000000000000000, 1.000000000000000000, 0.000000000000000000 ) ) ;
#9353=AXIS2_PLACEMENT_3D ( 'NONE', #15639, #10977, #7793 ) ;
#9356=CARTESIAN_POINT ( 'NONE',  ( 498.8334540492693918, 167.8734308960555950, 0.000000000000000000 ) ) ;
#9361=AXIS2_PLACEMENT_3D ( 'NONE', #8860, #19568, #18027 ) ;
#9362=AXIS2_PLACEMENT_3D ( 'NONE', #2810, #20004, #4064 ) ;
#9368=VECTOR ( 'NONE', #15472, 1000.000000000000000 ) ;
#9371=PRESENTATION_STYLE_ASSIGNMENT (( #4844 ) ) ;
#9378=EDGE_LOOP ( 'NONE', ( #9792, #8732, #17865, #2999 ) ) ;
#9387=( NAMED_UNIT ( * ) SI_UNIT ( $, .STERADIAN. ) SOLID_ANGLE_UNIT ( ) );
#9406=EDGE_CURVE ( 'NONE', #6967, #16566, #8351, .T. ) ;
#9437=DIRECTION ( 'NONE',  ( 1.000000000000000000, 0.000000000000000000, 0.000000000000000000 ) ) ;
#9442=DIRECTION ( 'NONE',  ( 0.000000000000000000, 0.000000000000000000, -1.000000000000000000 ) ) ;
#9445=DIRECTION ( 'NONE',  ( 1.000000000000000000, 0.000000000000000000, -0.000000000000000000 ) ) ;
#9489=PRESENTATION_STYLE_ASSIGNMENT (( #18758 ) ) ;
#9493=ORIENTED_EDGE ( 'NONE', *, *, #6071, .F. ) ;
#9528=( GEOMETRIC_REPRESENTATION_CONTEXT ( 3 ) GLOBAL_UNCERTAINTY_ASSIGNED_CONTEXT ( ( #3997 ) ) GLOBAL_UNIT_ASSIGNED_CONTEXT ( ( #9155, #15560, #14096 ) ) REPRESENTATION_CONTEXT ( 'NONE', 'WORKASPACE' ) );
#9534=DIRECTION ( 'NONE',  ( 0.000000000000000000, 0.000000000000000000, -1.000000000000000000 ) ) ;
#9541=EDGE_CURVE ( 'NONE', #12426, #17668, #3833, .T. ) ;
#9545=STYLED_ITEM ( 'NONE', ( #3317 ), #6042 ) ;
#9547=SURFACE_STYLE_FILL_AREA ( #1697 ) ;
#9554=PRESENTATION_STYLE_ASSIGNMENT (( #15563 ) ) ;
#9555=DIRECTION ( 'NONE',  ( 1.000000000000000000, -0.000000000000000000, -0.000000000000000000 ) ) ;
#9561=DIRECTION ( 'NONE',  ( 1.000000000000000000, 0.000000000000000000, 0.000000000000000000 ) ) ;
#9567=ORIENTED_EDGE ( 'NONE', *, *, #4514, .F. ) ;
#9571=CARTESIAN_POINT ( 'NONE',  ( 503.8334540492693918, 167.8734308960555950, 0.000000000000000000 ) ) ;
#9577=LINE ( 'NONE', #11133, #8812 ) ;
#9591=( NAMED_UNIT ( * ) PLANE_ANGLE_UNIT ( ) SI_UNIT ( $, .RADIAN. ) );
#9612=EDGE_CURVE ( 'NONE', #12998, #886, #9100, .T. ) ;
#9613=COLOUR_RGB ( '', 0.72549020, 0.75294118, 0.79215686) ;
#9623=ORIENTED_EDGE ( 'NONE', *, *, #4733, .F. ) ;
#9634=STYLED_ITEM ( 'NONE', ( #939 ), #8501 ) ;
#9650=ORIENTED_EDGE ( 'NONE', *, *, #15713, .F. ) ;
#9651=DIRECTION ( 'NONE',  ( 1.000000000000000000, -0.000000000000000000, -0.000000000000000000 ) ) ;
#9668=STYLED_ITEM ( 'NONE', ( #1278 ), #7987 ) ;
#9671=CARTESIAN_POINT ( 'NONE',  ( 503.8334540492693918, 242.8734308960556234, 0.000000000000000000 ) ) ;
#9672=CARTESIAN_POINT ( 'NONE',  ( 423.8334540492694487, 191.8198460455371333, 168.2339398819845826 ) ) ;
#9678=DIRECTION ( 'NONE',  ( 1.000000000000000000, -0.000000000000000000, -0.000000000000000000 ) ) ;
#9679=ORIENTED_EDGE ( 'NONE', *, *, #2040, .F. ) ;
#9686=SURFACE_STYLE_FILL_AREA ( #3406 ) ;
#9687=LINE ( 'NONE', #6502, #14131 ) ;
#9695=FILL_AREA_STYLE ('',( #3413 ) ) ;
#9712=MECHANICAL_DESIGN_GEOMETRIC_PRESENTATION_REPRESENTATION('',(#16640),#822);
#9719=FILL_AREA_STYLE ('',( #3434 ) ) ;
#9721=LINE ( 'NONE', #14357, #1881 ) ;
#9722=VECTOR ( 'NONE', #12718, 1000.000000000000000 ) ;
#9728=LINE ( 'NONE', #19082, #18110 ) ;
#9734=VERTEX_POINT ( 'NONE', #19247 ) ;
#9739=SURFACE_STYLE_USAGE ( .BOTH. , #18129 ) ;
#9748=SURFACE_STYLE_USAGE ( .BOTH. , #1480 ) ;
#9759=CYLINDRICAL_SURFACE ( 'NONE', #20043, 10.00000000000000888 ) ;
#9770=ORIENTED_EDGE ( 'NONE', *, *, #2185, .F. ) ;
#9771=DIRECTION ( 'NONE',  ( 0.000000000000000000, 0.000000000000000000, -1.000000000000000000 ) ) ;
#9792=ORIENTED_EDGE ( 'NONE', *, *, #1249, .T. ) ;
#9795=FILL_AREA_STYLE ('',( #19155 ) ) ;
#9800=DIRECTION ( 'NONE',  ( 1.000000000000000000, -0.000000000000000000, -0.000000000000000000 ) ) ;
#9802=( NAMED_UNIT ( * ) PLANE_ANGLE_UNIT ( ) SI_UNIT ( $, .RADIAN. ) );
#9824=LINE ( 'NONE', #2068, #20217 ) ;
#9833=EDGE_CURVE ( 'NONE', #19270, #716, #770, .T. ) ;
#9840=CARTESIAN_POINT ( 'NONE',  ( 423.8334540492694487, 191.8198460455371333, 34.99421986894476788 ) ) ;
#9845=SURFACE_SIDE_STYLE ('',( #563 ) ) ;
#9849=FILL_AREA_STYLE ('',( #9953 ) ) ;
#9859=( NAMED_UNIT ( * ) PLANE_ANGLE_UNIT ( ) SI_UNIT ( $, .RADIAN. ) );
#9863=COLOUR_RGB ( '', 0.40784314, 0.44705882, 0.49803922) ;
#9864=CARTESIAN_POINT ( 'NONE',  ( 463.8334540492693350, 191.8198460455371333, 34.99421986894476788 ) ) ;
#9889=LINE ( 'NONE', #2029, #17885 ) ;
#9891=SURFACE_SIDE_STYLE ('',( #3517 ) ) ;
#9938=FILL_AREA_STYLE_COLOUR ( '', #9083 ) ;
#9953=FILL_AREA_STYLE_COLOUR ( '', #8635 ) ;
#9954=AXIS2_PLACEMENT_3D ( 'NONE', #11523, #19437, #17802 ) ;
#9980=ORIENTED_EDGE ( 'NONE', *, *, #18070, .F. ) ;
#9990=EDGE_CURVE ( 'NONE', #16566, #17444, #2844, .T. ) ;
#9993=CARTESIAN_POINT ( 'NONE',  ( 458.8334540492693350, 167.8734308960555950, 250.0000000000000000 ) ) ;
#9995=AXIS2_PLACEMENT_3D ( 'NONE', #6879, #18069, #19231 ) ;
#10022=VECTOR ( 'NONE', #18460, 1000.000000000000000 ) ;
#10030=SURFACE_STYLE_FILL_AREA ( #3745 ) ;
#10044=AXIS2_PLACEMENT_3D ( 'NONE', #14248, #8186, #8081 ) ;
#10055=VECTOR ( 'NONE', #1352, 1000.000000000000000 ) ;
#10080=FILL_AREA_STYLE ('',( #11829 ) ) ;
#10090=ORIENTED_EDGE ( 'NONE', *, *, #6071, .T. ) ;
#10107=DIRECTION ( 'NONE',  ( 1.000000000000000000, -0.000000000000000000, -0.000000000000000000 ) ) ;
#10109=SURFACE_SIDE_STYLE ('',( #5376 ) ) ;
#10128=CARTESIAN_POINT ( 'NONE',  ( 423.8334540492694487, 191.8198460455371333, 225.0057801310552463 ) ) ;
#10130=EDGE_LOOP ( 'NONE', ( #17969, #16488, #4330, #12362 ) ) ;
#10134=EDGE_CURVE ( 'NONE', #8671, #12704, #17895, .T. ) ;
#10138=ORIENTED_EDGE ( 'NONE', *, *, #12267, .T. ) ;
#10154=EDGE_CURVE ( 'NONE', #10866, #4282, #4895, .T. ) ;
#10165=EDGE_CURVE ( 'NONE', #8072, #3481, #18550, .T. ) ;
#10183=EDGE_LOOP ( 'NONE', ( #12372, #5956, #18840, #2529 ) ) ;
#10197=SURFACE_STYLE_FILL_AREA ( #8858 ) ;
#10199=VECTOR ( 'NONE', #10344, 1000.000000000000000 ) ;
#10202=ORIENTED_EDGE ( 'NONE', *, *, #15949, .T. ) ;
#10208=FILL_AREA_STYLE_COLOUR ( '', #19849 ) ;
#10209=CIRCLE ( 'NONE', #7225, 10.00000000000000888 ) ;
#10225=MECHANICAL_DESIGN_GEOMETRIC_PRESENTATION_REPRESENTATION('',(#5905),#13162);
#10227=CARTESIAN_POINT ( 'NONE',  ( 463.8334540492693350, 191.8198460455371333, 168.2339398819845826 ) ) ;
#10234=VECTOR ( 'NONE', #19440, 1000.000000000000000 ) ;
#10249=EDGE_CURVE ( 'NONE', #13105, #8449, #20198, .T. ) ;
#10251=PRESENTATION_STYLE_ASSIGNMENT (( #18074 ) ) ;
#10266=EDGE_CURVE ( 'NONE', #8092, #1837, #15293, .T. ) ;
#10302=CARTESIAN_POINT ( 'NONE',  ( 423.8334540492694487, 191.8198460455371333, 225.0057801310552463 ) ) ;
#10310=EDGE_LOOP ( 'NONE', ( #13386, #14137, #18209, #19746 ) ) ;
#10320=CARTESIAN_POINT ( 'NONE',  ( 498.8334540492693918, 191.8198460455371333, 178.2339398819846110 ) ) ;
#10344=DIRECTION ( 'NONE',  ( 1.000000000000000000, 0.000000000000000000, 0.000000000000000000 ) ) ;
#10349=FILL_AREA_STYLE_COLOUR ( '', #18510 ) ;
#10360=VECTOR ( 'NONE', #17046, 1000.000000000000000 ) ;
#10366=AXIS2_PLACEMENT_3D ( 'NONE', #1109, #14962, #4331 ) ;
#10379=DIRECTION ( 'NONE',  ( 0.000000000000000000, 0.000000000000000000, -1.000000000000000000 ) ) ;
#10386=DIRECTION ( 'NONE',  ( 0.000000000000000000, -1.000000000000000000, 0.000000000000000000 ) ) ;
#10393=CARTESIAN_POINT ( 'NONE',  ( 423.8334540492694487, 191.8198460455371333, 215.0057801310552179 ) ) ;
#10397=DIRECTION ( 'NONE',  ( 1.000000000000000000, 0.000000000000000000, 0.000000000000000000 ) ) ;
#10407=CIRCLE ( 'NONE', #18936, 10.00000000000000888 ) ;
#10408=CARTESIAN_POINT ( 'NONE',  ( 458.8334540492693350, 191.8198460455371333, 14.99421986894475012 ) ) ;
#10418=CIRCLE ( 'NONE', #4830, 10.00000000000000888 ) ;
#10423=FILL_AREA_STYLE_COLOUR ( '', #1127 ) ;
#10427=FACE_OUTER_BOUND ( 'NONE', #14894, .T. ) ;
#10431=LINE ( 'NONE', #11778, #19499 ) ;
#10437=VERTEX_POINT ( 'NONE', #4661 ) ;
#10449=CARTESIAN_POINT ( 'NONE',  ( 498.8334540492693918, 167.8734308960555950, 250.0000000000000000 ) ) ;
#10464=ORIENTED_EDGE ( 'NONE', *, *, #17713, .F. ) ;
#10468=DIRECTION ( 'NONE',  ( 1.000000000000000000, 0.000000000000000000, -0.000000000000000000 ) ) ;
#10480=FILL_AREA_STYLE ('',( #10583 ) ) ;
#10491=( NAMED_UNIT ( * ) PLANE_ANGLE_UNIT ( ) SI_UNIT ( $, .RADIAN. ) );
#10492=AXIS2_PLACEMENT_3D ( 'NONE', #19224, #6668, #6459 ) ;
#10501=CYLINDRICAL_SURFACE ( 'NONE', #20062, 10.00000000000000888 ) ;
#10502=SURFACE_SIDE_STYLE ('',( #10197 ) ) ;
#10513=SURFACE_STYLE_FILL_AREA ( #828 ) ;
#10524=SURFACE_SIDE_STYLE ('',( #13814 ) ) ;
#10534=( NAMED_UNIT ( * ) SI_UNIT ( $, .STERADIAN. ) SOLID_ANGLE_UNIT ( ) );
#10543=UNCERTAINTY_MEASURE_WITH_UNIT (LENGTH_MEASURE( 1.000000000000000082E-05 ), #9171, 'distance_accuracy_value', 'NONE');
#10579=CARTESIAN_POINT ( 'NONE',  ( 493.8117674897343363, 134.2156642432025251, 245.0000000000000000 ) ) ;
#10583=FILL_AREA_STYLE_COLOUR ( '', #20101 ) ;
#10587=ORIENTED_EDGE ( 'NONE', *, *, #14645, .F. ) ;
#10590=CARTESIAN_POINT ( 'NONE',  ( 503.8334540492693918, 191.8198460455371333, 225.0057801310552463 ) ) ;
#10592=DIRECTION ( 'NONE',  ( 0.000000000000000000, -0.000000000000000000, 1.000000000000000000 ) ) ;
#10601=FACE_OUTER_BOUND ( 'NONE', #11076, .T. ) ;
#10615=ORIENTED_EDGE ( 'NONE', *, *, #7811, .F. ) ;
#10623=CIRCLE ( 'NONE', #1722, 10.00000000000000888 ) ;
#10629=EDGE_CURVE ( 'NONE', #2872, #12998, #14098, .T. ) ;
#10635=VECTOR ( 'NONE', #16114, 1000.000000000000000 ) ;
#10638=CIRCLE ( 'NONE', #432, 10.00000000000000888 ) ;
#10643=CARTESIAN_POINT ( 'NONE',  ( 498.8117674897343932, 191.8198460455371333, 168.2339398819845826 ) ) ;
#10653=FACE_OUTER_BOUND ( 'NONE', #18360, .T. ) ;
#10657=ORIENTED_EDGE ( 'NONE', *, *, #2864, .T. ) ;
#10670=EDGE_LOOP ( 'NONE', ( #8510, #12913, #6802, #16745 ) ) ;
#10679=EDGE_CURVE ( 'NONE', #951, #2425, #20236, .T. ) ;
#10683=DIRECTION ( 'NONE',  ( 1.000000000000000000, 0.000000000000000000, -0.000000000000000000 ) ) ;
#10686=FACE_OUTER_BOUND ( 'NONE', #11100, .T. ) ;
#10689=( NAMED_UNIT ( * ) SI_UNIT ( $, .STERADIAN. ) SOLID_ANGLE_UNIT ( ) );
#10692=( GEOMETRIC_REPRESENTATION_CONTEXT ( 3 ) GLOBAL_UNCERTAINTY_ASSIGNED_CONTEXT ( ( #5192 ) ) GLOBAL_UNIT_ASSIGNED_CONTEXT ( ( #13425, #11868, #16811 ) ) REPRESENTATION_CONTEXT ( 'NONE', 'WORKASPACE' ) );
#10706=PRESENTATION_STYLE_ASSIGNMENT (( #4416 ) ) ;
#10710=FACE_OUTER_BOUND ( 'NONE', #11770, .T. ) ;
#10716=CYLINDRICAL_SURFACE ( 'NONE', #16143, 10.00000000000000888 ) ;
#10723=ORIENTED_EDGE ( 'NONE', *, *, #3718, .T. ) ;
#10728=UNCERTAINTY_MEASURE_WITH_UNIT (LENGTH_MEASURE( 1.000000000000000082E-05 ), #4843, 'distance_accuracy_value', 'NONE');
#10734=EDGE_CURVE ( 'NONE', #11175, #13635, #10807, .T. ) ;
#10750=SURFACE_STYLE_USAGE ( .BOTH. , #2607 ) ;
#10767=ORIENTED_EDGE ( 'NONE', *, *, #672, .F. ) ;
#10785=PRESENTATION_STYLE_ASSIGNMENT (( #7895 ) ) ;
#10798=PRESENTATION_STYLE_ASSIGNMENT (( #3371 ) ) ;
#10805=FACE_BOUND ( 'NONE', #7849, .T. ) ;
#10807=LINE ( 'NONE', #17087, #19267 ) ;
#10813=SURFACE_SIDE_STYLE ('',( #6595 ) ) ;
#10842=ADVANCED_FACE ( 'NONE', ( #13392 ), #19630, .F. ) ;
#10852=DIRECTION ( 'NONE',  ( -1.000000000000000000, -0.000000000000000000, -0.000000000000000000 ) ) ;
#10859=SURFACE_STYLE_USAGE ( .BOTH. , #1657 ) ;
#10865=DIRECTION ( 'NONE',  ( 0.000000000000000000, 0.000000000000000000, 1.000000000000000000 ) ) ;
#10866=VERTEX_POINT ( 'NONE', #4204 ) ;
#10870=PRESENTATION_STYLE_ASSIGNMENT (( #14068 ) ) ;
#10879=LINE ( 'NONE', #1794, #14901 ) ;
#10882=DIRECTION ( 'NONE',  ( 0.000000000000000000, -0.000000000000000000, 1.000000000000000000 ) ) ;
#10886=LINE ( 'NONE', #1363, #6005 ) ;
#10889=( NAMED_UNIT ( * ) SI_UNIT ( $, .STERADIAN. ) SOLID_ANGLE_UNIT ( ) );
#10898=EDGE_CURVE ( 'NONE', #7254, #15257, #3275, .T. ) ;
#10909=CARTESIAN_POINT ( 'NONE',  ( 498.8117674897343932, 134.2156642432025251, -2.775557561562891351E-14 ) ) ;
#10920=ORIENTED_EDGE ( 'NONE', *, *, #14532, .T. ) ;
#10921=DIRECTION ( 'NONE',  ( 0.000000000000000000, 0.000000000000000000, -1.000000000000000000 ) ) ;
#10935=ADVANCED_FACE ( 'NONE', ( #17567 ), #7798, .F. ) ;
#10944=ORIENTED_EDGE ( 'NONE', *, *, #19651, .T. ) ;
#10956=LINE ( 'NONE', #15505, #773 ) ;
#10977=DIRECTION ( 'NONE',  ( 1.000000000000000000, 0.000000000000000000, -0.000000000000000000 ) ) ;
#10979=( NAMED_UNIT ( * ) PLANE_ANGLE_UNIT ( ) SI_UNIT ( $, .RADIAN. ) );
#10986=( GEOMETRIC_REPRESENTATION_CONTEXT ( 3 ) GLOBAL_UNCERTAINTY_ASSIGNED_CONTEXT ( ( #10543 ) ) GLOBAL_UNIT_ASSIGNED_CONTEXT ( ( #9171, #16728, #1304 ) ) REPRESENTATION_CONTEXT ( 'NONE', 'WORKASPACE' ) );
#10990=FACE_OUTER_BOUND ( 'NONE', #18382, .T. ) ;
#10992=CARTESIAN_POINT ( 'NONE',  ( 498.8117674897343932, 214.2156642432025251, -87.31255586191144857 ) ) ;
#10998=VECTOR ( 'NONE', #18138, 1000.000000000000000 ) ;
#11020=CARTESIAN_POINT ( 'NONE',  ( 463.8334540492693350, 191.8198460455371333, 158.2339398819845826 ) ) ;
#11022=AXIS2_PLACEMENT_3D ( 'NONE', #5334, #11726, #9771 ) ;
#11023=( NAMED_UNIT ( * ) SI_UNIT ( $, .STERADIAN. ) SOLID_ANGLE_UNIT ( ) );
#11024=DIRECTION ( 'NONE',  ( 0.000000000000000000, 0.000000000000000000, -1.000000000000000000 ) ) ;
#11033=EDGE_CURVE ( 'NONE', #3481, #3254, #5610, .T. ) ;
#11035=ORIENTED_EDGE ( 'NONE', *, *, #8657, .T. ) ;
#11043=ADVANCED_FACE ( 'NONE', ( #7176 ), #6781, .F. ) ;
#11050=FILL_AREA_STYLE ('',( #6514 ) ) ;
#11055=ORIENTED_EDGE ( 'NONE', *, *, #2522, .T. ) ;
#11066=LINE ( 'NONE', #18679, #8168 ) ;
#11073=LINE ( 'NONE', #2915, #3021 ) ;
#11076=EDGE_LOOP ( 'NONE', ( #10138, #14543, #16909, #20357 ) ) ;
#11093=FACE_BOUND ( 'NONE', #3062, .T. ) ;
#11097=ORIENTED_EDGE ( 'NONE', *, *, #19435, .T. ) ;
#11100=EDGE_LOOP ( 'NONE', ( #6517, #11035, #6862, #3834 ) ) ;
#11117=VECTOR ( 'NONE', #9555, 1000.000000000000000 ) ;
#11119=DIRECTION ( 'NONE',  ( 1.000000000000000000, -0.000000000000000000, -0.000000000000000000 ) ) ;
#11128=DIRECTION ( 'NONE',  ( 1.000000000000000000, -0.000000000000000000, -0.000000000000000000 ) ) ;
#11133=CARTESIAN_POINT ( 'NONE',  ( 423.8334540492694487, 191.8198460455371333, 14.99421986894475012 ) ) ;
#11139=( LENGTH_UNIT ( ) NAMED_UNIT ( * ) SI_UNIT ( .MILLI., .METRE. ) );
#11158=VERTEX_POINT ( 'NONE', #8077 ) ;
#11172=EDGE_CURVE ( 'NONE', #7874, #6793, #11066, .T. ) ;
#11175=VERTEX_POINT ( 'NONE', #1865 ) ;
#11179=( NAMED_UNIT ( * ) SI_UNIT ( $, .STERADIAN. ) SOLID_ANGLE_UNIT ( ) );
#11199=SURFACE_STYLE_USAGE ( .BOTH. , #18924 ) ;
#11216=VERTEX_POINT ( 'NONE', #7775 ) ;
#11217=UNCERTAINTY_MEASURE_WITH_UNIT (LENGTH_MEASURE( 1.000000000000000082E-05 ), #17449, 'distance_accuracy_value', 'NONE');
#11218=CARTESIAN_POINT ( 'NONE',  ( 423.8334540492694487, 191.8198460455371333, 91.76606011801541740 ) ) ;
#11238=( GEOMETRIC_REPRESENTATION_CONTEXT ( 3 ) GLOBAL_UNCERTAINTY_ASSIGNED_CONTEXT ( ( #1725 ) ) GLOBAL_UNIT_ASSIGNED_CONTEXT ( ( #15859, #3171, #12548 ) ) REPRESENTATION_CONTEXT ( 'NONE', 'WORKASPACE' ) );
#11240=DIRECTION ( 'NONE',  ( 0.000000000000000000, -1.000000000000000000, 0.000000000000000000 ) ) ;
#11248=CARTESIAN_POINT ( 'NONE',  ( 498.8117674897343932, 214.2156642432025251, -87.31255586191144857 ) ) ;
#11268=FILL_AREA_STYLE_COLOUR ( '', #17628 ) ;
#11274=DIRECTION ( 'NONE',  ( 0.000000000000000000, 1.000000000000000000, 0.000000000000000000 ) ) ;
#11294=ORIENTED_EDGE ( 'NONE', *, *, #17055, .F. ) ;
#11302=COLOUR_RGB ( '', 0.72549020, 0.75294118, 0.79215686) ;
#11303=EDGE_CURVE ( 'NONE', #14242, #17347, #9721, .T. ) ;
#11309=EDGE_CURVE ( 'NONE', #17347, #11940, #4570, .T. ) ;
#11312=( GEOMETRIC_REPRESENTATION_CONTEXT ( 3 ) GLOBAL_UNCERTAINTY_ASSIGNED_CONTEXT ( ( #5795 ) ) GLOBAL_UNIT_ASSIGNED_CONTEXT ( ( #17140, #16043, #1463 ) ) REPRESENTATION_CONTEXT ( 'NONE', 'WORKASPACE' ) );
#11336=VECTOR ( 'NONE', #9678, 1000.000000000000000 ) ;
#11365=AXIS2_PLACEMENT_3D ( 'NONE', #3035, #7887, #19222 ) ;
#11366=SURFACE_STYLE_USAGE ( .BOTH. , #327 ) ;
#11370=( NAMED_UNIT ( * ) PLANE_ANGLE_UNIT ( ) SI_UNIT ( $, .RADIAN. ) );
#11389=CARTESIAN_POINT ( 'NONE',  ( 493.8117674897343363, 214.2156642432025251, 245.0000000000000000 ) ) ;
#11401=SURFACE_SIDE_STYLE ('',( #5522 ) ) ;
#11441=PLANE ( 'NONE',  #6390 ) ;
#11442=( NAMED_UNIT ( * ) PLANE_ANGLE_UNIT ( ) SI_UNIT ( $, .RADIAN. ) );
#11452=LINE ( 'NONE', #17515, #3111 ) ;
#11465=DIRECTION ( 'NONE',  ( 1.000000000000000000, 0.000000000000000000, 0.000000000000000000 ) ) ;
#11483=LINE ( 'NONE', #9840, #13180 ) ;
#11485=DIRECTION ( 'NONE',  ( -0.000000000000000000, -0.000000000000000000, -1.000000000000000000 ) ) ;
#11496=SURFACE_STYLE_USAGE ( .BOTH. , #11401 ) ;
#11505=( LENGTH_UNIT ( ) NAMED_UNIT ( * ) SI_UNIT ( .MILLI., .METRE. ) );
#11506=CARTESIAN_POINT ( 'NONE',  ( 463.8334540492693350, 214.2156642432025251, 250.0000000000000000 ) ) ;
#11514=ORIENTED_EDGE ( 'NONE', *, *, #8091, .T. ) ;
#11523=CARTESIAN_POINT ( 'NONE',  ( 463.8334540492693350, 191.8198460455371333, 225.0057801310552463 ) ) ;
#11527=ORIENTED_EDGE ( 'NONE', *, *, #3685, .T. ) ;
#11545=LINE ( 'NONE', #3915, #16075 ) ;
#11546=DIRECTION ( 'NONE',  ( 1.000000000000000000, -0.000000000000000000, -0.000000000000000000 ) ) ;
#11548=STYLED_ITEM ( 'NONE', ( #519 ), #11802 ) ;
#11557=UNCERTAINTY_MEASURE_WITH_UNIT (LENGTH_MEASURE( 1.000000000000000082E-05 ), #4182, 'distance_accuracy_value', 'NONE');
#11566=CARTESIAN_POINT ( 'NONE',  ( 458.8334540492693350, 191.8198460455371333, 225.0057801310552463 ) ) ;
#11584=DIRECTION ( 'NONE',  ( 0.000000000000000000, 0.000000000000000000, 1.000000000000000000 ) ) ;
#11588=CARTESIAN_POINT ( 'NONE',  ( 503.8334540492693918, 167.8734308960555950, 250.0000000000000000 ) ) ;
#11595=SURFACE_STYLE_USAGE ( .BOTH. , #8312 ) ;
#11598=FACE_OUTER_BOUND ( 'NONE', #17053, .T. ) ;
#11606=ORIENTED_EDGE ( 'NONE', *, *, #18946, .T. ) ;
#11610=EDGE_LOOP ( 'NONE', ( #1379, #14162 ) ) ;
#11629=VECTOR ( 'NONE', #4619, 1000.000000000000000 ) ;
#11636=VERTEX_POINT ( 'NONE', #4652 ) ;
#11637=CARTESIAN_POINT ( 'NONE',  ( 486.8117674897343363, 134.2156642432025251, 245.0000000000000000 ) ) ;
#11653=CARTESIAN_POINT ( 'NONE',  ( 423.8334540492694487, 191.8198460455371333, 178.2339398819846110 ) ) ;
#11673=VECTOR ( 'NONE', #1891, 1000.000000000000000 ) ;
#11676=DIRECTION ( 'NONE',  ( 0.000000000000000000, -1.000000000000000000, 0.000000000000000000 ) ) ;
#11687=COLOUR_RGB ( '', 0.66274510, 0.83137255, 0.94901961) ;
#11689=ADVANCED_FACE ( 'NONE', ( #4762 ), #9281, .F. ) ;
#11694=PLANE ( 'NONE',  #15345 ) ;
#11699=DIRECTION ( 'NONE',  ( 1.000000000000000000, -0.000000000000000000, -0.000000000000000000 ) ) ;
#11720=CIRCLE ( 'NONE', #2809, 10.00000000000000888 ) ;
#11726=DIRECTION ( 'NONE',  ( 1.000000000000000000, -0.000000000000000000, -0.000000000000000000 ) ) ;
#11731=MECHANICAL_DESIGN_GEOMETRIC_PRESENTATION_REPRESENTATION('',(#16672),#7771);
#11753=FACE_BOUND ( 'NONE', #5323, .T. ) ;
#11767=SURFACE_SIDE_STYLE ('',( #10513 ) ) ;
#11768=UNCERTAINTY_MEASURE_WITH_UNIT (LENGTH_MEASURE( 1.000000000000000082E-05 ), #7591, 'distance_accuracy_value', 'NONE');
#11770=EDGE_LOOP ( 'NONE', ( #19017, #3119, #6429, #1875 ) ) ;
#11773=UNCERTAINTY_MEASURE_WITH_UNIT (LENGTH_MEASURE( 1.000000000000000082E-05 ), #17007, 'distance_accuracy_value', 'NONE');
#11778=CARTESIAN_POINT ( 'NONE',  ( 468.8334540492694487, 134.2156642432025251, 245.0000000000000000 ) ) ;
#11795=EDGE_LOOP ( 'NONE', ( #17812, #384 ) ) ;
#11798=VERTEX_POINT ( 'NONE', #13016 ) ;
#11802=ADVANCED_FACE ( 'NONE', ( #2156 ), #19164, .F. ) ;
#11806=CARTESIAN_POINT ( 'NONE',  ( 468.8334540492694487, 214.2156642432025251, 245.0000000000000000 ) ) ;
#11808=LINE ( 'NONE', #17876, #8187 ) ;
#11824=PRESENTATION_STYLE_ASSIGNMENT (( #18085 ) ) ;
#11829=FILL_AREA_STYLE_COLOUR ( '', #2786 ) ;
#11838=UNCERTAINTY_MEASURE_WITH_UNIT (LENGTH_MEASURE( 1.000000000000000082E-05 ), #12358, 'distance_accuracy_value', 'NONE');
#11839=FILL_AREA_STYLE_COLOUR ( '', #1666 ) ;
#11843=ORIENTED_EDGE ( 'NONE', *, *, #6243, .F. ) ;
#11847=( GEOMETRIC_REPRESENTATION_CONTEXT ( 3 ) GLOBAL_UNCERTAINTY_ASSIGNED_CONTEXT ( ( #2403 ) ) GLOBAL_UNIT_ASSIGNED_CONTEXT ( ( #3894, #7496, #17069 ) ) REPRESENTATION_CONTEXT ( 'NONE', 'WORKASPACE' ) );
#11848=ORIENTED_EDGE ( 'NONE', *, *, #1677, .T. ) ;
#11853=( NAMED_UNIT ( * ) SI_UNIT ( $, .STERADIAN. ) SOLID_ANGLE_UNIT ( ) );
#11861=( NAMED_UNIT ( * ) PLANE_ANGLE_UNIT ( ) SI_UNIT ( $, .RADIAN. ) );
#11868=( NAMED_UNIT ( * ) PLANE_ANGLE_UNIT ( ) SI_UNIT ( $, .RADIAN. ) );
#11869=ORIENTED_EDGE ( 'NONE', *, *, #2185, .T. ) ;
#11877=DIRECTION ( 'NONE',  ( 1.000000000000000000, 0.000000000000000000, 0.000000000000000000 ) ) ;
#11879=ADVANCED_FACE ( 'NONE', ( #9071 ), #7434, .F. ) ;
#11883=CARTESIAN_POINT ( 'NONE',  ( 468.8334540492694487, 214.2156642432025251, 245.0000000000000000 ) ) ;
#11898=ORIENTED_EDGE ( 'NONE', *, *, #6278, .T. ) ;
#11901=FACE_OUTER_BOUND ( 'NONE', #18210, .T. ) ;
#11939=LINE ( 'NONE', #18208, #20227 ) ;
#11940=VERTEX_POINT ( 'NONE', #8209 ) ;
#11942=STYLED_ITEM ( 'NONE', ( #1994 ), #18267 ) ;
#11960=CARTESIAN_POINT ( 'NONE',  ( 423.8334540492694487, 191.8198460455371333, 158.2339398819845826 ) ) ;
#11963=PRESENTATION_STYLE_ASSIGNMENT (( #19659 ) ) ;
#11983=( LENGTH_UNIT ( ) NAMED_UNIT ( * ) SI_UNIT ( .MILLI., .METRE. ) );
#11986=FILL_AREA_STYLE ('',( #2499 ) ) ;
#11995=UNCERTAINTY_MEASURE_WITH_UNIT (LENGTH_MEASURE( 1.000000000000000082E-05 ), #6608, 'distance_accuracy_value', 'NONE');
#12025=CIRCLE ( 'NONE', #17934, 10.00000000000000888 ) ;
#12027=VECTOR ( 'NONE', #17677, 1000.000000000000000 ) ;
#12029=CIRCLE ( 'NONE', #10366, 10.00000000000000888 ) ;
#12037=FACE_OUTER_BOUND ( 'NONE', #8065, .T. ) ;
#12059=ORIENTED_EDGE ( 'NONE', *, *, #10249, .F. ) ;
#12072=FACE_OUTER_BOUND ( 'NONE', #10670, .T. ) ;
#12084=PRESENTATION_STYLE_ASSIGNMENT (( #5989 ) ) ;
#12089=CARTESIAN_POINT ( 'NONE',  ( 463.8334540492693350, 214.2156642432025251, 250.0000000000000000 ) ) ;
#12090=EDGE_LOOP ( 'NONE', ( #15206, #8579, #19403, #11898 ) ) ;
#12096=ORIENTED_EDGE ( 'NONE', *, *, #14296, .T. ) ;
#12109=SURFACE_SIDE_STYLE ('',( #9118 ) ) ;
#12131=CARTESIAN_POINT ( 'NONE',  ( 0.000000000000000000, 0.000000000000000000, 250.0000000000000000 ) ) ;
#12157=VECTOR ( 'NONE', #13193, 1000.000000000000000 ) ;
#12158=( GEOMETRIC_REPRESENTATION_CONTEXT ( 3 ) GLOBAL_UNCERTAINTY_ASSIGNED_CONTEXT ( ( #11838 ) ) GLOBAL_UNIT_ASSIGNED_CONTEXT ( ( #12358, #15358, #7818 ) ) REPRESENTATION_CONTEXT ( 'NONE', 'WORKASPACE' ) );
#12170=DIRECTION ( 'NONE',  ( 0.000000000000000000, -0.000000000000000000, 1.000000000000000000 ) ) ;
#12171=AXIS2_PLACEMENT_3D ( 'NONE', #2512, #15088, #19497 ) ;
#12177=SURFACE_SIDE_STYLE ('',( #15387 ) ) ;
#12188=FACE_OUTER_BOUND ( 'NONE', #7977, .T. ) ;
#12200=ORIENTED_EDGE ( 'NONE', *, *, #14435, .T. ) ;
#12205=EDGE_LOOP ( 'NONE', ( #5110, #16398, #5704, #12973 ) ) ;
#12207=MECHANICAL_DESIGN_GEOMETRIC_PRESENTATION_REPRESENTATION('',(#2997),#19121);
#12216=ADVANCED_FACE ( 'NONE', ( #10710 ), #6384, .F. ) ;
#12219=DIRECTION ( 'NONE',  ( 0.000000000000000000, 0.000000000000000000, -1.000000000000000000 ) ) ;
#12225=SURFACE_STYLE_USAGE ( .BOTH. , #8931 ) ;
#12234=VECTOR ( 'NONE', #1973, 1000.000000000000000 ) ;
#12241=FACE_OUTER_BOUND ( 'NONE', #15734, .T. ) ;
#12251=FILL_AREA_STYLE ('',( #16905 ) ) ;
#12267=EDGE_CURVE ( 'NONE', #8092, #7872, #3087, .T. ) ;
#12278=VERTEX_POINT ( 'NONE', #17703 ) ;
#12279=SURFACE_STYLE_USAGE ( .BOTH. , #12177 ) ;
#12280=CIRCLE ( 'NONE', #8009, 10.00000000000000888 ) ;
#12308=VERTEX_POINT ( 'NONE', #16086 ) ;
#12312=COLOUR_RGB ( '', 0.08235294, 0.09019608, 0.10196078) ;
#12333=SURFACE_STYLE_FILL_AREA ( #18709 ) ;
#12347=EDGE_CURVE ( 'NONE', #13802, #886, #14809, .T. ) ;
#12349=DIRECTION ( 'NONE',  ( -0.000000000000000000, 0.000000000000000000, 1.000000000000000000 ) ) ;
#12356=SURFACE_SIDE_STYLE ('',( #18634 ) ) ;
#12358=( LENGTH_UNIT ( ) NAMED_UNIT ( * ) SI_UNIT ( .MILLI., .METRE. ) );
#12362=ORIENTED_EDGE ( 'NONE', *, *, #12915, .F. ) ;
#12372=ORIENTED_EDGE ( 'NONE', *, *, #8450, .T. ) ;
#12375=ORIENTED_EDGE ( 'NONE', *, *, #1390, .T. ) ;
#12386=PRODUCT_DEFINITION_SHAPE ( 'NONE', 'NONE',  #8109 ) ;
#12390=PRESENTATION_STYLE_ASSIGNMENT (( #104 ) ) ;
#12399=VERTEX_POINT ( 'NONE', #8621 ) ;
#12426=VERTEX_POINT ( 'NONE', #3988 ) ;
#12436=DIRECTION ( 'NONE',  ( 1.000000000000000000, 0.000000000000000000, 0.000000000000000000 ) ) ;
#12441=FACE_BOUND ( 'NONE', #5925, .T. ) ;
#12457=PLANE ( 'NONE',  #15465 ) ;
#12461=( NAMED_UNIT ( * ) PLANE_ANGLE_UNIT ( ) SI_UNIT ( $, .RADIAN. ) );
#12472=LINE ( 'NONE', #7734, #9368 ) ;
#12474=ORIENTED_EDGE ( 'NONE', *, *, #12783, .T. ) ;
#12477=CYLINDRICAL_SURFACE ( 'NONE', #3994, 10.00000000000000888 ) ;
#12485=DIRECTION ( 'NONE',  ( 0.000000000000000000, 0.000000000000000000, -1.000000000000000000 ) ) ;
#12494=( GEOMETRIC_REPRESENTATION_CONTEXT ( 3 ) GLOBAL_UNCERTAINTY_ASSIGNED_CONTEXT ( ( #2335 ) ) GLOBAL_UNIT_ASSIGNED_CONTEXT ( ( #7424, #13307, #11853 ) ) REPRESENTATION_CONTEXT ( 'NONE', 'WORKASPACE' ) );
#12498=EDGE_CURVE ( 'NONE', #12308, #8243, #1361, .T. ) ;
#12513=AXIS2_PLACEMENT_3D ( 'NONE', #1860, #16125, #19471 ) ;
#12544=EDGE_CURVE ( 'NONE', #12308, #9734, #16364, .T. ) ;
#12548=( NAMED_UNIT ( * ) SI_UNIT ( $, .STERADIAN. ) SOLID_ANGLE_UNIT ( ) );
#12581=DIRECTION ( 'NONE',  ( -0.000000000000000000, -0.000000000000000000, 1.000000000000000000 ) ) ;
#12583=MECHANICAL_DESIGN_GEOMETRIC_PRESENTATION_REPRESENTATION('',(#5017),#15880);
#12593=( GEOMETRIC_REPRESENTATION_CONTEXT ( 3 ) GLOBAL_UNCERTAINTY_ASSIGNED_CONTEXT ( ( #19770 ) ) GLOBAL_UNIT_ASSIGNED_CONTEXT ( ( #19505, #17877, #5424 ) ) REPRESENTATION_CONTEXT ( 'NONE', 'WORKASPACE' ) );
#12609=MECHANICAL_DESIGN_GEOMETRIC_PRESENTATION_REPRESENTATION('',(#18508),#2715);
#12658=CARTESIAN_POINT ( 'NONE',  ( 486.8117674897343363, 214.2156642432025251, 245.0000000000000000 ) ) ;
#12663=EDGE_CURVE ( 'NONE', #6575, #716, #16548, .T. ) ;
#12677=CARTESIAN_POINT ( 'NONE',  ( 475.8334540492694487, 134.2156642432025251, 245.0000000000000000 ) ) ;
#12686=UNCERTAINTY_MEASURE_WITH_UNIT (LENGTH_MEASURE( 1.000000000000000082E-05 ), #16546, 'distance_accuracy_value', 'NONE');
#12701=( LENGTH_UNIT ( ) NAMED_UNIT ( * ) SI_UNIT ( .MILLI., .METRE. ) );
#12704=VERTEX_POINT ( 'NONE', #17979 ) ;
#12718=DIRECTION ( 'NONE',  ( 0.000000000000000000, 0.000000000000000000, 1.000000000000000000 ) ) ;
#12734=VERTEX_POINT ( 'NONE', #11806 ) ;
#12767=CARTESIAN_POINT ( 'NONE',  ( 463.8334540492693350, 134.2156642432025251, 250.0000000000000000 ) ) ;
#12782=( NAMED_UNIT ( * ) PLANE_ANGLE_UNIT ( ) SI_UNIT ( $, .RADIAN. ) );
#12783=EDGE_CURVE ( 'NONE', #10866, #11940, #7865, .T. ) ;
#12785=EDGE_LOOP ( 'NONE', ( #9266, #1636 ) ) ;
#12787=CARTESIAN_POINT ( 'NONE',  ( 498.8334540492693918, 214.2156642432025251, 0.000000000000000000 ) ) ;
#12793=CIRCLE ( 'NONE', #7202, 10.00000000000000888 ) ;
#12813=ORIENTED_EDGE ( 'NONE', *, *, #10, .F. ) ;
#12833=STYLED_ITEM ( 'NONE', ( #1933 ), #6418 ) ;
#12839=ORIENTED_EDGE ( 'NONE', *, *, #2038, .F. ) ;
#12849=PRESENTATION_STYLE_ASSIGNMENT (( #9748 ) ) ;
#12850=CIRCLE ( 'NONE', #4290, 10.00000000000000888 ) ;
#12856=CARTESIAN_POINT ( 'NONE',  ( 468.8334540492694487, 214.2156642432025251, 250.0000000000000000 ) ) ;
#12860=( NAMED_UNIT ( * ) SI_UNIT ( $, .STERADIAN. ) SOLID_ANGLE_UNIT ( ) );
#12868=DIRECTION ( 'NONE',  ( 0.000000000000000000, 1.000000000000000000, 0.000000000000000000 ) ) ;
#12891=VERTEX_POINT ( 'NONE', #13843 ) ;
#12900=CYLINDRICAL_SURFACE ( 'NONE', #1592, 10.00000000000000888 ) ;
#12913=ORIENTED_EDGE ( 'NONE', *, *, #6504, .T. ) ;
#12915=EDGE_CURVE ( 'NONE', #3837, #15261, #9824, .T. ) ;
#12916=CARTESIAN_POINT ( 'NONE',  ( 503.8334540492693918, 191.8198460455371333, 14.99421986894475012 ) ) ;
#12921=ORIENTED_EDGE ( 'NONE', *, *, #14532, .F. ) ;
#12924=DIRECTION ( 'NONE',  ( 0.000000000000000000, 0.000000000000000000, -1.000000000000000000 ) ) ;
#12928=SURFACE_SIDE_STYLE ('',( #10030 ) ) ;
#12931=AXIS2_PLACEMENT_3D ( 'NONE', #17067, #2535, #10379 ) ;
#12939=ORIENTED_EDGE ( 'NONE', *, *, #5597, .T. ) ;
#12944=MECHANICAL_DESIGN_GEOMETRIC_PRESENTATION_REPRESENTATION('',(#6686),#18832);
#12950=( LENGTH_UNIT ( ) NAMED_UNIT ( * ) SI_UNIT ( .MILLI., .METRE. ) );
#12963=PLANE ( 'NONE',  #19162 ) ;
#12966=SURFACE_STYLE_FILL_AREA ( #2110 ) ;
#12967=EDGE_CURVE ( 'NONE', #1279, #12891, #18912, .T. ) ;
#12973=ORIENTED_EDGE ( 'NONE', *, *, #18334, .T. ) ;
#12976=DIRECTION ( 'NONE',  ( 0.000000000000000000, 1.000000000000000000, 0.000000000000000000 ) ) ;
#12977=COLOUR_RGB ( '', 0.66274510, 0.83137255, 0.94901961) ;
#12998=VERTEX_POINT ( 'NONE', #19388 ) ;
#13008=( LENGTH_UNIT ( ) NAMED_UNIT ( * ) SI_UNIT ( .MILLI., .METRE. ) );
#13010=VECTOR ( 'NONE', #11240, 1000.000000000000000 ) ;
#13016=CARTESIAN_POINT ( 'NONE',  ( 458.8334540492693350, 167.8734308960555950, 0.000000000000000000 ) ) ;
#13036=VECTOR ( 'NONE', #6053, 1000.000000000000000 ) ;
#13044=CIRCLE ( 'NONE', #14330, 10.00000000000000888 ) ;
#13045=DIRECTION ( 'NONE',  ( 0.000000000000000000, 0.000000000000000000, -1.000000000000000000 ) ) ;
#13056=EDGE_CURVE ( 'NONE', #12734, #13149, #922, .T. ) ;
#13069=LINE ( 'NONE', #19404, #18263 ) ;
#13074=CARTESIAN_POINT ( 'NONE',  ( 423.8334540492694487, 191.8198460455371333, 225.0057801310552463 ) ) ;
#13080=( NAMED_UNIT ( * ) PLANE_ANGLE_UNIT ( ) SI_UNIT ( $, .RADIAN. ) );
#13092=SURFACE_STYLE_FILL_AREA ( #3273 ) ;
#13104=SURFACE_STYLE_USAGE ( .BOTH. , #14620 ) ;
#13105=VERTEX_POINT ( 'NONE', #16343 ) ;
#13114=( NAMED_UNIT ( * ) SI_UNIT ( $, .STERADIAN. ) SOLID_ANGLE_UNIT ( ) );
#13126=ORIENTED_EDGE ( 'NONE', *, *, #14923, .T. ) ;
#13131=ORIENTED_EDGE ( 'NONE', *, *, #691, .F. ) ;
#13149=VERTEX_POINT ( 'NONE', #15681 ) ;
#13154=DIRECTION ( 'NONE',  ( -1.000000000000000000, 0.000000000000000000, 0.000000000000000000 ) ) ;
#13162=( GEOMETRIC_REPRESENTATION_CONTEXT ( 3 ) GLOBAL_UNCERTAINTY_ASSIGNED_CONTEXT ( ( #14849 ) ) GLOBAL_UNIT_ASSIGNED_CONTEXT ( ( #1512, #12782, #14105 ) ) REPRESENTATION_CONTEXT ( 'NONE', 'WORKASPACE' ) );
#13170=VERTEX_POINT ( 'NONE', #11020 ) ;
#13180=VECTOR ( 'NONE', #16056, 1000.000000000000000 ) ;
#13184=SURFACE_STYLE_FILL_AREA ( #10080 ) ;
#13185=EDGE_CURVE ( 'NONE', #2425, #951, #7648, .T. ) ;
#13193=DIRECTION ( 'NONE',  ( -0.000000000000000000, -0.000000000000000000, -1.000000000000000000 ) ) ;
#13208=( GEOMETRIC_REPRESENTATION_CONTEXT ( 3 ) GLOBAL_UNCERTAINTY_ASSIGNED_CONTEXT ( ( #9085 ) ) GLOBAL_UNIT_ASSIGNED_CONTEXT ( ( #5198, #11370, #3642 ) ) REPRESENTATION_CONTEXT ( 'NONE', 'WORKASPACE' ) );
#13219=ORIENTED_EDGE ( 'NONE', *, *, #16578, .F. ) ;
#13225=CARTESIAN_POINT ( 'NONE',  ( 463.8334540492693350, 214.2156642432025251, 0.000000000000000000 ) ) ;
#13248=LINE ( 'NONE', #750, #16322 ) ;
#13262=MECHANICAL_DESIGN_GEOMETRIC_PRESENTATION_REPRESENTATION('',(#7982),#16505);
#13269=DIRECTION ( 'NONE',  ( 0.000000000000000000, -1.000000000000000000, 0.000000000000000000 ) ) ;
#13298=CLOSED_SHELL ( 'NONE', ( #19856, #17398, #8611, #16082, #6418, #8670, #6042, #827, #13886, #8244, #19583, #219, #7987, #7851, #10842, #1960, #6530, #9261, #12216, #11802, #16097, #18833, #11879, #1151, #15140, #11043 ) ) ;
#13299=VERTEX_POINT ( 'NONE', #12089 ) ;
#13307=( NAMED_UNIT ( * ) PLANE_ANGLE_UNIT ( ) SI_UNIT ( $, .RADIAN. ) );
#13315=( GEOMETRIC_REPRESENTATION_CONTEXT ( 3 ) GLOBAL_UNCERTAINTY_ASSIGNED_CONTEXT ( ( #5600 ) ) GLOBAL_UNIT_ASSIGNED_CONTEXT ( ( #12950, #6658, #4030 ) ) REPRESENTATION_CONTEXT ( 'NONE', 'WORKASPACE' ) );
#13319=ORIENTED_EDGE ( 'NONE', *, *, #13938, .T. ) ;
#13338=EDGE_CURVE ( 'NONE', #4150, #3254, #16552, .T. ) ;
#13354=ORIENTED_EDGE ( 'NONE', *, *, #10154, .F. ) ;
#13361=DIRECTION ( 'NONE',  ( 1.000000000000000000, 1.197852309262419498E-15, -0.000000000000000000 ) ) ;
#13369=DIRECTION ( 'NONE',  ( 1.000000000000000000, -0.000000000000000000, -0.000000000000000000 ) ) ;
#13373=DIRECTION ( 'NONE',  ( 0.000000000000000000, 0.000000000000000000, -1.000000000000000000 ) ) ;
#13386=ORIENTED_EDGE ( 'NONE', *, *, #4825, .F. ) ;
#13387=CARTESIAN_POINT ( 'NONE',  ( 463.8334540492693350, 191.8198460455371333, 225.0057801310552463 ) ) ;
#13388=PRESENTATION_STYLE_ASSIGNMENT (( #15423 ) ) ;
#13392=FACE_OUTER_BOUND ( 'NONE', #19689, .T. ) ;
#13405=VERTEX_POINT ( 'NONE', #16479 ) ;
#13412=DIRECTION ( 'NONE',  ( 0.000000000000000000, 0.000000000000000000, -1.000000000000000000 ) ) ;
#13420=DIRECTION ( 'NONE',  ( 1.000000000000000000, 1.197852309262419498E-15, -0.000000000000000000 ) ) ;
#13425=( LENGTH_UNIT ( ) NAMED_UNIT ( * ) SI_UNIT ( .MILLI., .METRE. ) );
#13430=DIRECTION ( 'NONE',  ( 0.000000000000000000, 0.000000000000000000, -1.000000000000000000 ) ) ;
#13437=CARTESIAN_POINT ( 'NONE',  ( 423.8334540492694487, 191.8198460455371333, 81.76606011801540319 ) ) ;
#13450=EDGE_CURVE ( 'NONE', #16176, #18080, #7973, .T. ) ;
#13456=CARTESIAN_POINT ( 'NONE',  ( 503.8334540492693918, 242.8734308960556234, 250.0000000000000000 ) ) ;
#13459=DIRECTION ( 'NONE',  ( 1.197852309262419498E-15, -1.000000000000000000, 0.000000000000000000 ) ) ;
#13463=DIRECTION ( 'NONE',  ( -0.000000000000000000, -0.000000000000000000, 1.000000000000000000 ) ) ;
#13466=( NAMED_UNIT ( * ) PLANE_ANGLE_UNIT ( ) SI_UNIT ( $, .RADIAN. ) );
#13492=EDGE_LOOP ( 'NONE', ( #11606, #19665, #15662, #12375, #5675, #12839, #11294, #8006, #4882, #2208, #9567, #14727 ) ) ;
#13500=DIRECTION ( 'NONE',  ( 0.000000000000000000, 0.000000000000000000, -1.000000000000000000 ) ) ;
#13508=MECHANICAL_DESIGN_GEOMETRIC_PRESENTATION_REPRESENTATION('',(#9545),#7253);
#13526=PRESENTATION_STYLE_ASSIGNMENT (( #919 ) ) ;
#13529=CARTESIAN_POINT ( 'NONE',  ( 0.000000000000000000, 0.000000000000000000, 0.000000000000000000 ) ) ;
#13533=EDGE_CURVE ( 'NONE', #11798, #13911, #8625, .T. ) ;
#13543=( NAMED_UNIT ( * ) PLANE_ANGLE_UNIT ( ) SI_UNIT ( $, .RADIAN. ) );
#13581=VERTEX_POINT ( 'NONE', #13874 ) ;
#13601=SURFACE_STYLE_USAGE ( .BOTH. , #13793 ) ;
#13602=DIRECTION ( 'NONE',  ( 0.000000000000000000, 0.000000000000000000, -1.000000000000000000 ) ) ;
#13605=CLOSED_SHELL ( 'NONE', ( #16547, #10935, #11689, #16487, #17188, #239, #5118, #17431, #18267, #15540, #8501, #6592, #9032, #8607, #19037, #1009, #18171, #17816, #14951, #2497, #7742, #6510 ) ) ;
#13613=SURFACE_STYLE_FILL_AREA ( #8405 ) ;
#13615=UNCERTAINTY_MEASURE_WITH_UNIT (LENGTH_MEASURE( 1.000000000000000082E-05 ), #2939, 'distance_accuracy_value', 'NONE');
#13620=AXIS2_PLACEMENT_3D ( 'NONE', #4804, #6551, #17451 ) ;
#13629=MECHANICAL_DESIGN_GEOMETRIC_PRESENTATION_REPRESENTATION('',(#17291),#8385);
#13632=ORIENTED_EDGE ( 'NONE', *, *, #3740, .T. ) ;
#13634=UNCERTAINTY_MEASURE_WITH_UNIT (LENGTH_MEASURE( 1.000000000000000082E-05 ), #14941, 'distance_accuracy_value', 'NONE');
#13635=VERTEX_POINT ( 'NONE', #18803 ) ;
#13659=VERTEX_POINT ( 'NONE', #7806 ) ;
#13667=ORIENTED_EDGE ( 'NONE', *, *, #5776, .T. ) ;
#13671=ORIENTED_EDGE ( 'NONE', *, *, #13907, .T. ) ;
#13675=FILL_AREA_STYLE ('',( #18087 ) ) ;
#13712=CARTESIAN_POINT ( 'NONE',  ( 423.8334540492694487, 191.8198460455371333, 81.76606011801540319 ) ) ;
#13713=CARTESIAN_POINT ( 'NONE',  ( 493.8117674897343363, 134.2156642432025251, 245.0000000000000000 ) ) ;
#13724=FILL_AREA_STYLE_COLOUR ( '', #1150 ) ;
#13726=( NAMED_UNIT ( * ) SI_UNIT ( $, .STERADIAN. ) SOLID_ANGLE_UNIT ( ) );
#13768=EDGE_CURVE ( 'NONE', #11636, #11158, #6699, .T. ) ;
#13777=ORIENTED_EDGE ( 'NONE', *, *, #1044, .T. ) ;
#13782=DIRECTION ( 'NONE',  ( 1.000000000000000000, 0.000000000000000000, 0.000000000000000000 ) ) ;
#13786=COLOUR_RGB ( '', 0.40784314, 0.44705882, 0.49803922) ;
#13788=FACE_BOUND ( 'NONE', #12785, .T. ) ;
#13790=DIRECTION ( 'NONE',  ( 1.000000000000000000, -0.000000000000000000, -0.000000000000000000 ) ) ;
#13793=SURFACE_SIDE_STYLE ('',( #15050 ) ) ;
#13801=AXIS2_PLACEMENT_3D ( 'NONE', #5846, #7688, #5744 ) ;
#13802=VERTEX_POINT ( 'NONE', #8381 ) ;
#13813=COLOUR_RGB ( '', 0.31764706, 0.68627451, 0.89019608) ;
#13814=SURFACE_STYLE_FILL_AREA ( #1422 ) ;
#13824=ORIENTED_EDGE ( 'NONE', *, *, #13056, .F. ) ;
#13831=VERTEX_POINT ( 'NONE', #5390 ) ;
#13842=STYLED_ITEM ( 'NONE', ( #6087 ), #16082 ) ;
#13843=CARTESIAN_POINT ( 'NONE',  ( 503.8334540492693918, 191.8198460455371333, 158.2339398819845826 ) ) ;
#13848=SURFACE_STYLE_FILL_AREA ( #7568 ) ;
#13855=ORIENTED_EDGE ( 'NONE', *, *, #8400, .T. ) ;
#13858=MECHANICAL_DESIGN_GEOMETRIC_PRESENTATION_REPRESENTATION('',(#3992),#5640);
#13863=( NAMED_UNIT ( * ) SI_UNIT ( $, .STERADIAN. ) SOLID_ANGLE_UNIT ( ) );
#13874=CARTESIAN_POINT ( 'NONE',  ( 475.8334540492694487, 214.2156642432025251, 245.0000000000000000 ) ) ;
#13886=ADVANCED_FACE ( 'NONE', ( #17532 ), #5087, .T. ) ;
#13907=EDGE_CURVE ( 'NONE', #12891, #1279, #12280, .T. ) ;
#13911=VERTEX_POINT ( 'NONE', #15380 ) ;
#13918=DIRECTION ( 'NONE',  ( 0.000000000000000000, 0.000000000000000000, -1.000000000000000000 ) ) ;
#13925=( NAMED_UNIT ( * ) SI_UNIT ( $, .STERADIAN. ) SOLID_ANGLE_UNIT ( ) );
#13938=EDGE_CURVE ( 'NONE', #13149, #17286, #10431, .T. ) ;
#13948=STYLED_ITEM ( 'NONE', ( #5170 ), #7851 ) ;
#13958=ORIENTED_EDGE ( 'NONE', *, *, #6356, .F. ) ;
#13967=CIRCLE ( 'NONE', #8058, 10.00000000000001066 ) ;
#13969=DIRECTION ( 'NONE',  ( 1.000000000000000000, 0.000000000000000000, 0.000000000000000000 ) ) ;
#13974=VECTOR ( 'NONE', #17496, 1000.000000000000000 ) ;
#13977=CARTESIAN_POINT ( 'NONE',  ( 503.8334540492693918, 191.8198460455371333, 235.0057801310552463 ) ) ;
#13988=COLOUR_RGB ( '', 0.09019608, 0.27058824, 0.51372549) ;
#14014=CYLINDRICAL_SURFACE ( 'NONE', #20082, 10.00000000000000888 ) ;
#14018=EDGE_LOOP ( 'NONE', ( #17292, #1381 ) ) ;
#14028=( NAMED_UNIT ( * ) PLANE_ANGLE_UNIT ( ) SI_UNIT ( $, .RADIAN. ) );
#14034=LINE ( 'NONE', #6307, #5377 ) ;
#14041=SURFACE_STYLE_FILL_AREA ( #11050 ) ;
#14049=SURFACE_STYLE_USAGE ( .BOTH. , #14136 ) ;
#14063=ORIENTED_EDGE ( 'NONE', *, *, #2864, .F. ) ;
#14068=SURFACE_STYLE_USAGE ( .BOTH. , #246 ) ;
#14096=( NAMED_UNIT ( * ) SI_UNIT ( $, .STERADIAN. ) SOLID_ANGLE_UNIT ( ) );
#14098=LINE ( 'NONE', #4317, #4136 ) ;
#14103=DIRECTION ( 'NONE',  ( 0.000000000000000000, 0.000000000000000000, -1.000000000000000000 ) ) ;
#14105=( NAMED_UNIT ( * ) SI_UNIT ( $, .STERADIAN. ) SOLID_ANGLE_UNIT ( ) );
#14121=AXIS2_PLACEMENT_3D ( 'NONE', #701, #16795, #13500 ) ;
#14131=VECTOR ( 'NONE', #8460, 1000.000000000000000 ) ;
#14136=SURFACE_SIDE_STYLE ('',( #17428 ) ) ;
#14137=ORIENTED_EDGE ( 'NONE', *, *, #12347, .T. ) ;
#14160=DIRECTION ( 'NONE',  ( -1.000000000000000000, 0.000000000000000000, 0.000000000000000000 ) ) ;
#14162=ORIENTED_EDGE ( 'NONE', *, *, #843, .F. ) ;
#14171=( NAMED_UNIT ( * ) PLANE_ANGLE_UNIT ( ) SI_UNIT ( $, .RADIAN. ) );
#14178=( NAMED_UNIT ( * ) SI_UNIT ( $, .STERADIAN. ) SOLID_ANGLE_UNIT ( ) );
#14194=COLOUR_RGB ( '', 0.08235294, 0.09019608, 0.10196078) ;
#14217=FACE_OUTER_BOUND ( 'NONE', #20126, .T. ) ;
#14242=VERTEX_POINT ( 'NONE', #18611 ) ;
#14248=CARTESIAN_POINT ( 'NONE',  ( 503.8334540492693918, 191.8198460455371333, 168.2339398819845826 ) ) ;
#14261=( NAMED_UNIT ( * ) SI_UNIT ( $, .STERADIAN. ) SOLID_ANGLE_UNIT ( ) );
#14267=CYLINDRICAL_SURFACE ( 'NONE', #4076, 10.00000000000001066 ) ;
#14272=EDGE_CURVE ( 'NONE', #3837, #11175, #5382, .T. ) ;
#14274=VECTOR ( 'NONE', #393, 1000.000000000000000 ) ;
#14280=FACE_BOUND ( 'NONE', #18083, .T. ) ;
#14295=FILL_AREA_STYLE ('',( #18629 ) ) ;
#14296=EDGE_CURVE ( 'NONE', #2872, #13802, #167, .T. ) ;
#14302=DIRECTION ( 'NONE',  ( -1.000000000000000000, 0.000000000000000000, 0.000000000000000000 ) ) ;
#14306=( GEOMETRIC_REPRESENTATION_CONTEXT ( 3 ) GLOBAL_UNCERTAINTY_ASSIGNED_CONTEXT ( ( #616 ) ) GLOBAL_UNIT_ASSIGNED_CONTEXT ( ( #11139, #15709, #19167 ) ) REPRESENTATION_CONTEXT ( 'NONE', 'WORKASPACE' ) );
#14307=EDGE_CURVE ( 'NONE', #6883, #5981, #8406, .T. ) ;
#14313=AXIS2_PLACEMENT_3D ( 'NONE', #16698, #19845, #5762 ) ;
#14319=ORIENTED_EDGE ( 'NONE', *, *, #2038, .T. ) ;
#14324=UNCERTAINTY_MEASURE_WITH_UNIT (LENGTH_MEASURE( 1.000000000000000082E-05 ), #19246, 'distance_accuracy_value', 'NONE');
#14330=AXIS2_PLACEMENT_3D ( 'NONE', #10227, #2386, #8690 ) ;
#14357=CARTESIAN_POINT ( 'NONE',  ( 498.8117674897343932, 214.2156642432025251, 250.0000000000000000 ) ) ;
#14361=ORIENTED_EDGE ( 'NONE', *, *, #17321, .T. ) ;
#14390=( NAMED_UNIT ( * ) PLANE_ANGLE_UNIT ( ) SI_UNIT ( $, .RADIAN. ) );
#14406=CARTESIAN_POINT ( 'NONE',  ( 503.8334540492693918, 191.8198460455371333, 91.76606011801541740 ) ) ;
#14423=ORIENTED_EDGE ( 'NONE', *, *, #13338, .F. ) ;
#14435=EDGE_CURVE ( 'NONE', #8449, #13105, #3799, .T. ) ;
#14462=APPLICATION_CONTEXT ( 'automotive_design' ) ;
#14470=FACE_BOUND ( 'NONE', #730, .T. ) ;
#14471=PRESENTATION_STYLE_ASSIGNMENT (( #9739 ) ) ;
#14488=ORIENTED_EDGE ( 'NONE', *, *, #4070, .T. ) ;
#14505=CARTESIAN_POINT ( 'NONE',  ( 498.8117674897343932, 191.8198460455371333, 235.0057801310552463 ) ) ;
#14511=CARTESIAN_POINT ( 'NONE',  ( 498.8117674897343932, 214.2156642432025251, 250.0000000000000000 ) ) ;
#14516=ORIENTED_EDGE ( 'NONE', *, *, #9237, .T. ) ;
#14523=( NAMED_UNIT ( * ) SI_UNIT ( $, .STERADIAN. ) SOLID_ANGLE_UNIT ( ) );
#14530=EDGE_CURVE ( 'NONE', #13299, #6793, #13248, .T. ) ;
#14532=EDGE_CURVE ( 'NONE', #6793, #16010, #5607, .T. ) ;
#14537=MECHANICAL_DESIGN_GEOMETRIC_PRESENTATION_REPRESENTATION('',(#19783),#6978);
#14543=ORIENTED_EDGE ( 'NONE', *, *, #7351, .T. ) ;
#14564=ORIENTED_EDGE ( 'NONE', *, *, #7811, .T. ) ;
#14583=DIRECTION ( 'NONE',  ( 0.000000000000000000, 0.000000000000000000, 1.000000000000000000 ) ) ;
#14591=SURFACE_SIDE_STYLE ('',( #12966 ) ) ;
#14609=CARTESIAN_POINT ( 'NONE',  ( 423.8334540492694487, 191.8198460455371333, 34.99421986894476788 ) ) ;
#14615=AXIS2_PLACEMENT_3D ( 'NONE', #4312, #7606, #10592 ) ;
#14617=MECHANICAL_DESIGN_GEOMETRIC_PRESENTATION_REPRESENTATION('',(#3095),#9344);
#14620=SURFACE_SIDE_STYLE ('',( #16394 ) ) ;
#14624=AXIS2_PLACEMENT_3D ( 'NONE', #10590, #13782, #7212 ) ;
#14640=STYLED_ITEM ( 'NONE', ( #11824 ), #827 ) ;
#14645=EDGE_CURVE ( 'NONE', #8331, #12278, #2610, .T. ) ;
#14649=STYLED_ITEM ( 'NONE', ( #16513 ), #1960 ) ;
#14689=ORIENTED_EDGE ( 'NONE', *, *, #5776, .F. ) ;
#14723=CARTESIAN_POINT ( 'NONE',  ( 423.8334540492694487, 191.8198460455371333, 91.76606011801541740 ) ) ;
#14727=ORIENTED_EDGE ( 'NONE', *, *, #13938, .F. ) ;
#14747=CARTESIAN_POINT ( 'NONE',  ( 498.8117674897343932, 191.8198460455371333, 215.0057801310552179 ) ) ;
#14755=LINE ( 'NONE', #14857, #186 ) ;
#14769=DIRECTION ( 'NONE',  ( 1.000000000000000000, 0.000000000000000000, -0.000000000000000000 ) ) ;
#14770=( GEOMETRIC_REPRESENTATION_CONTEXT ( 3 ) GLOBAL_UNCERTAINTY_ASSIGNED_CONTEXT ( ( #3759 ) ) GLOBAL_UNIT_ASSIGNED_CONTEXT ( ( #7160, #4350, #10534 ) ) REPRESENTATION_CONTEXT ( 'NONE', 'WORKASPACE' ) );
#14783=DIRECTION ( 'NONE',  ( 0.000000000000000000, -1.000000000000000000, 0.000000000000000000 ) ) ;
#14790=AXIS2_PLACEMENT_3D ( 'NONE', #16874, #9227, #10882 ) ;
#14809=LINE ( 'NONE', #14609, #18538 ) ;
#14821=EDGE_LOOP ( 'NONE', ( #8751, #2511, #10723, #8110 ) ) ;
#14826=EDGE_CURVE ( 'NONE', #12399, #6575, #5090, .T. ) ;
#14836=DIRECTION ( 'NONE',  ( 0.000000000000000000, 0.000000000000000000, -1.000000000000000000 ) ) ;
#14840=( GEOMETRIC_REPRESENTATION_CONTEXT ( 3 ) GLOBAL_UNCERTAINTY_ASSIGNED_CONTEXT ( ( #3736 ) ) GLOBAL_UNIT_ASSIGNED_CONTEXT ( ( #8161, #9802, #1943 ) ) REPRESENTATION_CONTEXT ( 'NONE', 'WORKASPACE' ) );
#14849=UNCERTAINTY_MEASURE_WITH_UNIT (LENGTH_MEASURE( 1.000000000000000082E-05 ), #1512, 'distance_accuracy_value', 'NONE');
#14856=EDGE_LOOP ( 'NONE', ( #10767, #1222 ) ) ;
#14857=CARTESIAN_POINT ( 'NONE',  ( 423.8334540492694487, 191.8198460455371333, 71.76606011801538898 ) ) ;
#14860=VECTOR ( 'NONE', #760, 1000.000000000000000 ) ;
#14865=( GEOMETRIC_REPRESENTATION_CONTEXT ( 3 ) GLOBAL_UNCERTAINTY_ASSIGNED_CONTEXT ( ( #5051 ) ) GLOBAL_UNIT_ASSIGNED_CONTEXT ( ( #7262, #13543, #2399 ) ) REPRESENTATION_CONTEXT ( 'NONE', 'WORKASPACE' ) );
#14883=DIRECTION ( 'NONE',  ( 0.000000000000000000, 0.000000000000000000, -1.000000000000000000 ) ) ;
#14892=CYLINDRICAL_SURFACE ( 'NONE', #9995, 10.00000000000000888 ) ;
#14894=EDGE_LOOP ( 'NONE', ( #6257, #14319, #5910, #15513 ) ) ;
#14895=CARTESIAN_POINT ( 'NONE',  ( 463.8334540492693350, 191.8198460455371333, 91.76606011801541740 ) ) ;
#14901=VECTOR ( 'NONE', #9437, 1000.000000000000000 ) ;
#14922=PRESENTATION_STYLE_ASSIGNMENT (( #16693 ) ) ;
#14923=EDGE_CURVE ( 'NONE', #7205, #16010, #7340, .T. ) ;
#14927=CYLINDRICAL_SURFACE ( 'NONE', #9249, 10.00000000000000888 ) ;
#14928=CARTESIAN_POINT ( 'NONE',  ( 498.8334540492693918, 214.2156642432025251, 250.0000000000000000 ) ) ;
#14941=( LENGTH_UNIT ( ) NAMED_UNIT ( * ) SI_UNIT ( .MILLI., .METRE. ) );
#14944=FILL_AREA_STYLE ('',( #18324 ) ) ;
#14947=CARTESIAN_POINT ( 'NONE',  ( 458.8334540492693350, 191.8198460455371333, 24.99421986894476078 ) ) ;
#14951=ADVANCED_FACE ( 'NONE', ( #1012 ), #19890, .F. ) ;
#14961=AXIS2_PLACEMENT_3D ( 'NONE', #10992, #9445, #1581 ) ;
#14962=DIRECTION ( 'NONE',  ( 1.000000000000000000, 0.000000000000000000, -0.000000000000000000 ) ) ;
#14966=PLANE ( 'NONE',  #17231 ) ;
#14968=COLOUR_RGB ( '', 0.08235294, 0.09019608, 0.10196078) ;
#14971=CARTESIAN_POINT ( 'NONE',  ( 498.8334540492693918, 191.8198460455371333, 235.0057801310552463 ) ) ;
#14977=CARTESIAN_POINT ( 'NONE',  ( 463.8334540492693350, 214.2156642432025251, 0.000000000000000000 ) ) ;
#15008=ORIENTED_EDGE ( 'NONE', *, *, #9406, .F. ) ;
#15028=( LENGTH_UNIT ( ) NAMED_UNIT ( * ) SI_UNIT ( .MILLI., .METRE. ) );
#15050=SURFACE_STYLE_FILL_AREA ( #4138 ) ;
#15072=SURFACE_SIDE_STYLE ('',( #18551 ) ) ;
#15081=ORIENTED_EDGE ( 'NONE', *, *, #17713, .T. ) ;
#15088=DIRECTION ( 'NONE',  ( 1.000000000000000000, 0.000000000000000000, -0.000000000000000000 ) ) ;
#15090=SURFACE_SIDE_STYLE ('',( #8807 ) ) ;
#15111=ORIENTED_EDGE ( 'NONE', *, *, #11172, .T. ) ;
#15115=CARTESIAN_POINT ( 'NONE',  ( 463.8334540492693918, 167.8734308960555950, 250.0000000000000000 ) ) ;
#15116=CARTESIAN_POINT ( 'NONE',  ( 503.8334540492693918, 191.8198460455371333, 71.76606011801538898 ) ) ;
#15118=SURFACE_STYLE_USAGE ( .BOTH. , #19430 ) ;
#15132=STYLED_ITEM ( 'NONE', ( #1280 ), #6530 ) ;
#15140=ADVANCED_FACE ( 'NONE', ( #12188 ), #857, .F. ) ;
#15159=DIRECTION ( 'NONE',  ( 0.000000000000000000, 0.000000000000000000, -1.000000000000000000 ) ) ;
#15165=AXIS2_PLACEMENT_3D ( 'NONE', #13712, #2357, #5879 ) ;
#15175=CARTESIAN_POINT ( 'NONE',  ( 463.8334540492693350, 214.2156642432025251, 250.0000000000000000 ) ) ;
#15177=EDGE_CURVE ( 'NONE', #6967, #13170, #12025, .T. ) ;
#15188=( NAMED_UNIT ( * ) PLANE_ANGLE_UNIT ( ) SI_UNIT ( $, .RADIAN. ) );
#15195=LINE ( 'NONE', #7275, #1075 ) ;
#15198=ORIENTED_EDGE ( 'NONE', *, *, #15949, .F. ) ;
#15201=VERTEX_POINT ( 'NONE', #8075 ) ;
#15206=ORIENTED_EDGE ( 'NONE', *, *, #5756, .F. ) ;
#15213=PLANE ( 'NONE',  #84 ) ;
#15221=CARTESIAN_POINT ( 'NONE',  ( 475.8334540492694487, 134.2156642432025251, 245.0000000000000000 ) ) ;
#15232=ORIENTED_EDGE ( 'NONE', *, *, #13450, .T. ) ;
#15241=DIRECTION ( 'NONE',  ( -0.000000000000000000, 1.000000000000000000, -0.000000000000000000 ) ) ;
#15243=PRODUCT_DEFINITION_FORMATION_WITH_SPECIFIED_SOURCE ( 'ANY', '', #16206, .NOT_KNOWN. ) ;
#15257=VERTEX_POINT ( 'NONE', #15915 ) ;
#15261=VERTEX_POINT ( 'NONE', #7960 ) ;
#15267=( LENGTH_UNIT ( ) NAMED_UNIT ( * ) SI_UNIT ( .MILLI., .METRE. ) );
#15270=CARTESIAN_POINT ( 'NONE',  ( 406.3334540492693350, 242.8734308960556234, 250.0000000000000000 ) ) ;
#15274=DIRECTION ( 'NONE',  ( 1.000000000000000000, -0.000000000000000000, -0.000000000000000000 ) ) ;
#15293=LINE ( 'NONE', #1325, #10022 ) ;
#15297=AXIS2_PLACEMENT_3D ( 'NONE', #13437, #15274, #1120 ) ;
#15310=ORIENTED_EDGE ( 'NONE', *, *, #19947, .F. ) ;
#15311=ORIENTED_EDGE ( 'NONE', *, *, #1946, .T. ) ;
#15317=AXIS2_PLACEMENT_3D ( 'NONE', #3914, #12436, #14836 ) ;
#15325=EDGE_LOOP ( 'NONE', ( #15631, #581 ) ) ;
#15335=CARTESIAN_POINT ( 'NONE',  ( 463.8334540492693350, 191.8198460455371333, 235.0057801310552463 ) ) ;
#15338=( NAMED_UNIT ( * ) SI_UNIT ( $, .STERADIAN. ) SOLID_ANGLE_UNIT ( ) );
#15345=AXIS2_PLACEMENT_3D ( 'NONE', #7738, #7443, #3090 ) ;
#15353=LINE ( 'NONE', #1276, #17910 ) ;
#15356=ORIENTED_EDGE ( 'NONE', *, *, #9612, .F. ) ;
#15358=( NAMED_UNIT ( * ) PLANE_ANGLE_UNIT ( ) SI_UNIT ( $, .RADIAN. ) );
#15365=SURFACE_SIDE_STYLE ('',( #20175 ) ) ;
#15372=( NAMED_UNIT ( * ) SI_UNIT ( $, .STERADIAN. ) SOLID_ANGLE_UNIT ( ) );
#15380=CARTESIAN_POINT ( 'NONE',  ( 458.8334540492693350, 242.8734308960556234, 0.000000000000000000 ) ) ;
#15383=MANIFOLD_SOLID_BREP ( 'Cut-Extrude4[1]', #13298 ) ;
#15387=SURFACE_STYLE_FILL_AREA ( #11986 ) ;
#15388=DIRECTION ( 'NONE',  ( 0.000000000000000000, -1.000000000000000000, 0.000000000000000000 ) ) ;
#15408=PLANE ( 'NONE',  #3088 ) ;
#15422=( LENGTH_UNIT ( ) NAMED_UNIT ( * ) SI_UNIT ( .MILLI., .METRE. ) );
#15423=SURFACE_STYLE_USAGE ( .BOTH. , #5933 ) ;
#15434=SURFACE_STYLE_FILL_AREA ( #1688 ) ;
#15437=EDGE_CURVE ( 'NONE', #8671, #17668, #3993, .T. ) ;
#15453=SURFACE_STYLE_FILL_AREA ( #17004 ) ;
#15457=EDGE_CURVE ( 'NONE', #4282, #17048, #20145, .T. ) ;
#15463=FILL_AREA_STYLE_COLOUR ( '', #6578 ) ;
#15465=AXIS2_PLACEMENT_3D ( 'NONE', #1598, #7517, #20165 ) ;
#15470=EDGE_LOOP ( 'NONE', ( #1614, #12813 ) ) ;
#15472=DIRECTION ( 'NONE',  ( 1.000000000000000000, -0.000000000000000000, -0.000000000000000000 ) ) ;
#15474=ORIENTED_EDGE ( 'NONE', *, *, #16352, .F. ) ;
#15482=STYLED_ITEM ( 'NONE', ( #1810 ), #16487 ) ;
#15483=CARTESIAN_POINT ( 'NONE',  ( 498.8334540492693918, 191.8198460455371333, 24.99421986894476078 ) ) ;
#15491=LINE ( 'NONE', #18664, #18876 ) ;
#15505=CARTESIAN_POINT ( 'NONE',  ( 406.3334540492693350, 167.8734308960555950, 0.000000000000000000 ) ) ;
#15506=CARTESIAN_POINT ( 'NONE',  ( 463.8334540492693350, 191.8198460455371333, 168.2339398819845826 ) ) ;
#15513=ORIENTED_EDGE ( 'NONE', *, *, #11309, .T. ) ;
#15540=ADVANCED_FACE ( 'NONE', ( #11093, #14280, #12441, #15852, #10686 ), #4701, .T. ) ;
#15556=CARTESIAN_POINT ( 'NONE',  ( 463.8334540492693350, 191.8198460455371333, 215.0057801310552179 ) ) ;
#15559=EDGE_LOOP ( 'NONE', ( #14689, #1778, #11097, #20289 ) ) ;
#15560=( NAMED_UNIT ( * ) PLANE_ANGLE_UNIT ( ) SI_UNIT ( $, .RADIAN. ) );
#15563=SURFACE_STYLE_USAGE ( .BOTH. , #9253 ) ;
#15624=CARTESIAN_POINT ( 'NONE',  ( 0.000000000000000000, 0.000000000000000000, 245.0000000000000000 ) ) ;
#15631=ORIENTED_EDGE ( 'NONE', *, *, #8450, .F. ) ;
#15638=ORIENTED_EDGE ( 'NONE', *, *, #16578, .T. ) ;
#15639=CARTESIAN_POINT ( 'NONE',  ( 498.8334540492693918, 191.8198460455371333, 81.76606011801540319 ) ) ;
#15651=CARTESIAN_POINT ( 'NONE',  ( 498.8117674897343932, 191.8198460455371333, 225.0057801310552463 ) ) ;
#15654=SURFACE_SIDE_STYLE ('',( #15434 ) ) ;
#15662=ORIENTED_EDGE ( 'NONE', *, *, #12663, .F. ) ;
#15670=CARTESIAN_POINT ( 'NONE',  ( 498.8334540492693918, 191.8198460455371333, 91.76606011801541740 ) ) ;
#15672=PLANE ( 'NONE',  #3947 ) ;
#15681=CARTESIAN_POINT ( 'NONE',  ( 468.8334540492694487, 134.2156642432025251, 245.0000000000000000 ) ) ;
#15685=CARTESIAN_POINT ( 'NONE',  ( 463.8334540492693350, 191.8198460455371333, 215.0057801310552179 ) ) ;
#15695=SURFACE_SIDE_STYLE ('',( #13613 ) ) ;
#15704=SURFACE_SIDE_STYLE ('',( #1311 ) ) ;
#15709=( NAMED_UNIT ( * ) PLANE_ANGLE_UNIT ( ) SI_UNIT ( $, .RADIAN. ) );
#15713=EDGE_CURVE ( 'NONE', #6449, #7874, #15491, .T. ) ;
#15720=DIRECTION ( 'NONE',  ( 0.000000000000000000, 0.000000000000000000, -1.000000000000000000 ) ) ;
#15734=EDGE_LOOP ( 'NONE', ( #8152, #6888, #7528, #16301 ) ) ;
#15761=CARTESIAN_POINT ( 'NONE',  ( 463.8334540492693350, 214.2156642432025251, -87.31255586191144857 ) ) ;
#15767=FACE_BOUND ( 'NONE', #9276, .T. ) ;
#15825=ORIENTED_EDGE ( 'NONE', *, *, #1677, .F. ) ;
#15827=DIRECTION ( 'NONE',  ( 1.000000000000000000, 1.197852309262419498E-15, -0.000000000000000000 ) ) ;
#15846=COLOUR_RGB ( '', 0.08235294, 0.09019608, 0.10196078) ;
#15852=FACE_BOUND ( 'NONE', #15470, .T. ) ;
#15859=( LENGTH_UNIT ( ) NAMED_UNIT ( * ) SI_UNIT ( .MILLI., .METRE. ) );
#15871=COLOUR_RGB ( '', 0.40784314, 0.44705882, 0.49803922) ;
#15873=MANIFOLD_SOLID_BREP ( 'Cut-Extrude4[2]', #13605 ) ;
#15880=( GEOMETRIC_REPRESENTATION_CONTEXT ( 3 ) GLOBAL_UNCERTAINTY_ASSIGNED_CONTEXT ( ( #5985 ) ) GLOBAL_UNIT_ASSIGNED_CONTEXT ( ( #8719, #13466, #5621 ) ) REPRESENTATION_CONTEXT ( 'NONE', 'WORKASPACE' ) );
#15905=STYLED_ITEM ( 'NONE', ( #10785 ), #18171 ) ;
#15909=EDGE_CURVE ( 'NONE', #13635, #15261, #6424, .T. ) ;
#15911=( NAMED_UNIT ( * ) SI_UNIT ( $, .STERADIAN. ) SOLID_ANGLE_UNIT ( ) );
#15915=CARTESIAN_POINT ( 'NONE',  ( 503.8334540492693918, 191.8198460455371333, 34.99421986894476788 ) ) ;
#15946=MECHANICAL_DESIGN_GEOMETRIC_PRESENTATION_REPRESENTATION('',(#13948),#8999);
#15948=DIRECTION ( 'NONE',  ( 0.000000000000000000, -0.000000000000000000, 1.000000000000000000 ) ) ;
#15949=EDGE_CURVE ( 'NONE', #7872, #8092, #145, .T. ) ;
#15969=MECHANICAL_DESIGN_GEOMETRIC_PRESENTATION_REPRESENTATION('',(#18871),#11312);
#15974=EDGE_CURVE ( 'NONE', #6215, #1279, #1947, .T. ) ;
#15978=( NAMED_UNIT ( * ) PLANE_ANGLE_UNIT ( ) SI_UNIT ( $, .RADIAN. ) );
#16006=UNCERTAINTY_MEASURE_WITH_UNIT (LENGTH_MEASURE( 1.000000000000000082E-05 ), #18745, 'distance_accuracy_value', 'NONE');
#16010=VERTEX_POINT ( 'NONE', #8658 ) ;
#16011=CARTESIAN_POINT ( 'NONE',  ( 463.8334540492693350, 191.8198460455371333, 81.76606011801540319 ) ) ;
#16015=STYLED_ITEM ( 'NONE', ( #10870 ), #9032 ) ;
#16020=SURFACE_SIDE_STYLE ('',( #5472 ) ) ;
#16024=VERTEX_POINT ( 'NONE', #13713 ) ;
#16043=( NAMED_UNIT ( * ) PLANE_ANGLE_UNIT ( ) SI_UNIT ( $, .RADIAN. ) );
#16053=FILL_AREA_STYLE ('',( #11268 ) ) ;
#16054=ORIENTED_EDGE ( 'NONE', *, *, #14307, .T. ) ;
#16056=DIRECTION ( 'NONE',  ( 1.000000000000000000, -0.000000000000000000, -0.000000000000000000 ) ) ;
#16070=SURFACE_STYLE_USAGE ( .BOTH. , #14591 ) ;
#16075=VECTOR ( 'NONE', #16713, 1000.000000000000000 ) ;
#16077=CARTESIAN_POINT ( 'NONE',  ( 498.8117674897343932, 214.2156642432025251, 0.000000000000000000 ) ) ;
#16082=ADVANCED_FACE ( 'NONE', ( #7224 ), #10716, .F. ) ;
#16086=CARTESIAN_POINT ( 'NONE',  ( 475.8334540492694487, 134.2156642432025251, 250.0000000000000000 ) ) ;
#16094=FILL_AREA_STYLE ('',( #11839 ) ) ;
#16097=ADVANCED_FACE ( 'NONE', ( #8143 ), #14014, .F. ) ;
#16103=EDGE_LOOP ( 'NONE', ( #17639, #15081, #18436, #19467, #3667, #9493, #13126, #925 ) ) ;
#16106=SURFACE_STYLE_FILL_AREA ( #8459 ) ;
#16107=SURFACE_STYLE_USAGE ( .BOTH. , #9891 ) ;
#16114=DIRECTION ( 'NONE',  ( 0.000000000000000000, 1.000000000000000000, 0.000000000000000000 ) ) ;
#16125=DIRECTION ( 'NONE',  ( 1.000000000000000000, -0.000000000000000000, -0.000000000000000000 ) ) ;
#16143=AXIS2_PLACEMENT_3D ( 'NONE', #6489, #11119, #11024 ) ;
#16144=VECTOR ( 'NONE', #19751, 1000.000000000000000 ) ;
#16161=( NAMED_UNIT ( * ) PLANE_ANGLE_UNIT ( ) SI_UNIT ( $, .RADIAN. ) );
#16164=ORIENTED_EDGE ( 'NONE', *, *, #8657, .F. ) ;
#16165=DIRECTION ( 'NONE',  ( -0.000000000000000000, -0.000000000000000000, 1.000000000000000000 ) ) ;
#16168=( LENGTH_UNIT ( ) NAMED_UNIT ( * ) SI_UNIT ( .MILLI., .METRE. ) );
#16176=VERTEX_POINT ( 'NONE', #15685 ) ;
#16178=ORIENTED_EDGE ( 'NONE', *, *, #6356, .T. ) ;
#16180=AXIS2_PLACEMENT_3D ( 'NONE', #7750, #20302, #12485 ) ;
#16204=EDGE_CURVE ( 'NONE', #10437, #13831, #16295, .T. ) ;
#16206=PRODUCT ( 'Part11^Assem2', 'Part11^Assem2', '', ( #16853 ) ) ;
#16234=PRESENTATION_STYLE_ASSIGNMENT (( #19190 ) ) ;
#16250=VERTEX_POINT ( 'NONE', #18505 ) ;
#16252=DIRECTION ( 'NONE',  ( -1.000000000000000000, 0.000000000000000000, 0.000000000000000000 ) ) ;
#16255=DIRECTION ( 'NONE',  ( -0.000000000000000000, -0.000000000000000000, 1.000000000000000000 ) ) ;
#16274=( NAMED_UNIT ( * ) SI_UNIT ( $, .STERADIAN. ) SOLID_ANGLE_UNIT ( ) );
#16286=CARTESIAN_POINT ( 'NONE',  ( 423.8334540492694487, 191.8198460455371333, 81.76606011801540319 ) ) ;
#16295=LINE ( 'NONE', #14928, #12157 ) ;
#16301=ORIENTED_EDGE ( 'NONE', *, *, #9833, .F. ) ;
#16303=ORIENTED_EDGE ( 'NONE', *, *, #3671, .T. ) ;
#16322=VECTOR ( 'NONE', #13459, 1000.000000000000000 ) ;
#16337=VECTOR ( 'NONE', #11676, 1000.000000000000000 ) ;
#16343=CARTESIAN_POINT ( 'NONE',  ( 463.8334540492693350, 191.8198460455371333, 34.99421986894476788 ) ) ;
#16352=EDGE_CURVE ( 'NONE', #11636, #16176, #19945, .T. ) ;
#16354=AXIS2_PLACEMENT_3D ( 'NONE', #1115, #2787, #19986 ) ;
#16363=FILL_AREA_STYLE_COLOUR ( '', #1927 ) ;
#16364=LINE ( 'NONE', #564, #11673 ) ;
#16365=ORIENTED_EDGE ( 'NONE', *, *, #18334, .F. ) ;
#16369=CARTESIAN_POINT ( 'NONE',  ( 463.8334540492693350, 134.2156642432025251, -87.31255586191144857 ) ) ;
#16381=LINE ( 'NONE', #16077, #2349 ) ;
#16394=SURFACE_STYLE_FILL_AREA ( #16094 ) ;
#16398=ORIENTED_EDGE ( 'NONE', *, *, #12498, .T. ) ;
#16443=ORIENTED_EDGE ( 'NONE', *, *, #8400, .F. ) ;
#16449=DIRECTION ( 'NONE',  ( 0.000000000000000000, 0.000000000000000000, 1.000000000000000000 ) ) ;
#16479=CARTESIAN_POINT ( 'NONE',  ( 493.8117674897343363, 134.2156642432025251, 250.0000000000000000 ) ) ;
#16487=ADVANCED_FACE ( 'NONE', ( #19237 ), #9759, .F. ) ;
#16488=ORIENTED_EDGE ( 'NONE', *, *, #10734, .T. ) ;
#16505=( GEOMETRIC_REPRESENTATION_CONTEXT ( 3 ) GLOBAL_UNCERTAINTY_ASSIGNED_CONTEXT ( ( #7929 ) ) GLOBAL_UNIT_ASSIGNED_CONTEXT ( ( #12701, #1532, #13925 ) ) REPRESENTATION_CONTEXT ( 'NONE', 'WORKASPACE' ) );
#16506=DIRECTION ( 'NONE',  ( -1.000000000000000000, 0.000000000000000000, 0.000000000000000000 ) ) ;
#16507=CARTESIAN_POINT ( 'NONE',  ( 0.000000000000000000, 0.000000000000000000, 250.0000000000000000 ) ) ;
#16511=CIRCLE ( 'NONE', #18456, 10.00000000000000888 ) ;
#16512=VERTEX_POINT ( 'NONE', #8318 ) ;
#16513=PRESENTATION_STYLE_ASSIGNMENT (( #3922 ) ) ;
#16520=EDGE_LOOP ( 'NONE', ( #4536, #13319, #17328, #14564 ) ) ;
#16535=AXIS2_PLACEMENT_3D ( 'NONE', #9317, #3144, #20123 ) ;
#16546=( LENGTH_UNIT ( ) NAMED_UNIT ( * ) SI_UNIT ( .MILLI., .METRE. ) );
#16547=ADVANCED_FACE ( 'NONE', ( #10601 ), #10501, .F. ) ;
#16548=LINE ( 'NONE', #18279, #1434 ) ;
#16552=CIRCLE ( 'NONE', #2035, 10.00000000000000888 ) ;
#16566=VERTEX_POINT ( 'NONE', #5561 ) ;
#16578=EDGE_CURVE ( 'NONE', #11216, #12891, #5661, .T. ) ;
#16620=VECTOR ( 'NONE', #14160, 1000.000000000000000 ) ;
#16625=VECTOR ( 'NONE', #10107, 1000.000000000000000 ) ;
#16632=MECHANICAL_DESIGN_GEOMETRIC_PRESENTATION_REPRESENTATION('',(#14640),#1440);
#16640=STYLED_ITEM ( 'NONE', ( #14922 ), #15383 ) ;
#16649=AXIS2_PLACEMENT_3D ( 'NONE', #16903, #2764, #17006 ) ;
#16672=STYLED_ITEM ( 'NONE', ( #12084 ), #2497 ) ;
#16693=SURFACE_STYLE_USAGE ( .BOTH. , #20038 ) ;
#16698=CARTESIAN_POINT ( 'NONE',  ( 458.8334540492693350, 191.8198460455371333, 225.0057801310552463 ) ) ;
#16713=DIRECTION ( 'NONE',  ( 1.000000000000000000, -0.000000000000000000, -0.000000000000000000 ) ) ;
#16728=( NAMED_UNIT ( * ) PLANE_ANGLE_UNIT ( ) SI_UNIT ( $, .RADIAN. ) );
#16729=UNCERTAINTY_MEASURE_WITH_UNIT (LENGTH_MEASURE( 1.000000000000000082E-05 ), #16168, 'distance_accuracy_value', 'NONE');
#16745=ORIENTED_EDGE ( 'NONE', *, *, #5902, .T. ) ;
#16751=LINE ( 'NONE', #4358, #10199 ) ;
#16754=DIRECTION ( 'NONE',  ( 0.000000000000000000, 0.000000000000000000, 1.000000000000000000 ) ) ;
#16775=MECHANICAL_DESIGN_GEOMETRIC_PRESENTATION_REPRESENTATION('',(#3936),#12494);
#16794=SURFACE_STYLE_USAGE ( .BOTH. , #12356 ) ;
#16795=DIRECTION ( 'NONE',  ( 1.000000000000000000, -0.000000000000000000, -0.000000000000000000 ) ) ;
#16799=( GEOMETRIC_REPRESENTATION_CONTEXT ( 3 ) GLOBAL_UNCERTAINTY_ASSIGNED_CONTEXT ( ( #19370 ) ) GLOBAL_UNIT_ASSIGNED_CONTEXT ( ( #1095, #1194, #7522 ) ) REPRESENTATION_CONTEXT ( 'NONE', 'WORKASPACE' ) );
#16811=( NAMED_UNIT ( * ) SI_UNIT ( $, .STERADIAN. ) SOLID_ANGLE_UNIT ( ) );
#16844=FILL_AREA_STYLE ('',( #18366 ) ) ;
#16845=AXIS2_PLACEMENT_3D ( 'NONE', #15761, #9351, #6177 ) ;
#16853=PRODUCT_CONTEXT ( 'NONE', #14462, 'mechanical' ) ;
#16874=CARTESIAN_POINT ( 'NONE',  ( 498.8334540492693918, 167.8734308960555950, 250.0000000000000000 ) ) ;
#16879=DIRECTION ( 'NONE',  ( 1.000000000000000000, -0.000000000000000000, -0.000000000000000000 ) ) ;
#16903=CARTESIAN_POINT ( 'NONE',  ( 498.8334540492693918, 191.8198460455371333, 225.0057801310552463 ) ) ;
#16905=FILL_AREA_STYLE_COLOUR ( '', #14194 ) ;
#16909=ORIENTED_EDGE ( 'NONE', *, *, #6243, .T. ) ;
#16976=CARTESIAN_POINT ( 'NONE',  ( 486.8117674897343363, 134.2156642432025251, 250.0000000000000000 ) ) ;
#16979=DIRECTION ( 'NONE',  ( 0.000000000000000000, 0.000000000000000000, -1.000000000000000000 ) ) ;
#16995=ORIENTED_EDGE ( 'NONE', *, *, #4514, .T. ) ;
#16999=ORIENTED_EDGE ( 'NONE', *, *, #385, .F. ) ;
#17002=( LENGTH_UNIT ( ) NAMED_UNIT ( * ) SI_UNIT ( .MILLI., .METRE. ) );
#17004=FILL_AREA_STYLE ('',( #4524 ) ) ;
#17006=DIRECTION ( 'NONE',  ( 0.000000000000000000, 0.000000000000000000, -1.000000000000000000 ) ) ;
#17007=( LENGTH_UNIT ( ) NAMED_UNIT ( * ) SI_UNIT ( .MILLI., .METRE. ) );
#17011=SURFACE_STYLE_USAGE ( .BOTH. , #15365 ) ;
#17031=DIRECTION ( 'NONE',  ( 0.000000000000000000, 0.000000000000000000, -1.000000000000000000 ) ) ;
#17046=DIRECTION ( 'NONE',  ( -0.000000000000000000, -0.000000000000000000, 1.000000000000000000 ) ) ;
#17048=VERTEX_POINT ( 'NONE', #334 ) ;
#17053=EDGE_LOOP ( 'NONE', ( #17399, #17371, #18744, #15232 ) ) ;
#17055=EDGE_CURVE ( 'NONE', #16024, #13405, #9728, .T. ) ;
#17063=CARTESIAN_POINT ( 'NONE',  ( 423.8334540492694487, 191.8198460455371333, 34.99421986894476788 ) ) ;
#17067=CARTESIAN_POINT ( 'NONE',  ( 498.8334540492693918, 191.8198460455371333, 168.2339398819845826 ) ) ;
#17069=( NAMED_UNIT ( * ) SI_UNIT ( $, .STERADIAN. ) SOLID_ANGLE_UNIT ( ) );
#17087=CARTESIAN_POINT ( 'NONE',  ( 423.8334540492694487, 191.8198460455371333, 178.2339398819846110 ) ) ;
#17098=ORIENTED_EDGE ( 'NONE', *, *, #476, .F. ) ;
#17108=ORIENTED_EDGE ( 'NONE', *, *, #13185, .F. ) ;
#17117=VECTOR ( 'NONE', #18225, 1000.000000000000000 ) ;
#17120=ORIENTED_EDGE ( 'NONE', *, *, #5695, .T. ) ;
#17123=STYLED_ITEM ( 'NONE', ( #19656 ), #11879 ) ;
#17136=CARTESIAN_POINT ( 'NONE',  ( 493.8117674897343363, 214.2156642432025251, 245.0000000000000000 ) ) ;
#17140=( LENGTH_UNIT ( ) NAMED_UNIT ( * ) SI_UNIT ( .MILLI., .METRE. ) );
#17143=CARTESIAN_POINT ( 'NONE',  ( 463.8334540492693350, 191.8198460455371333, 24.99421986894476078 ) ) ;
#17148=MECHANICAL_DESIGN_GEOMETRIC_PRESENTATION_REPRESENTATION('',(#2671),#7609);
#17173=ORIENTED_EDGE ( 'NONE', *, *, #14923, .F. ) ;
#17183=SURFACE_SIDE_STYLE ('',( #15453 ) ) ;
#17188=ADVANCED_FACE ( 'NONE', ( #12072 ), #7524, .T. ) ;
#17189=LINE ( 'NONE', #19021, #11117 ) ;
#17228=VERTEX_POINT ( 'NONE', #9671 ) ;
#17229=( GEOMETRIC_REPRESENTATION_CONTEXT ( 3 ) GLOBAL_UNCERTAINTY_ASSIGNED_CONTEXT ( ( #8895 ) ) GLOBAL_UNIT_ASSIGNED_CONTEXT ( ( #18791, #10979, #11179 ) ) REPRESENTATION_CONTEXT ( 'NONE', 'WORKASPACE' ) );
#17231=AXIS2_PLACEMENT_3D ( 'NONE', #7144, #13430, #19668 ) ;
#17264=LINE ( 'NONE', #17063, #10055 ) ;
#17284=ORIENTED_EDGE ( 'NONE', *, *, #14272, .F. ) ;
#17286=VERTEX_POINT ( 'NONE', #12677 ) ;
#17287=FACE_OUTER_BOUND ( 'NONE', #18884, .T. ) ;
#17291=STYLED_ITEM ( 'NONE', ( #13526 ), #14951 ) ;
#17292=ORIENTED_EDGE ( 'NONE', *, *, #14272, .T. ) ;
#17294=FACE_BOUND ( 'NONE', #4172, .T. ) ;
#17308=EDGE_LOOP ( 'NONE', ( #16443, #7714, #5690, #4795 ) ) ;
#17316=VECTOR ( 'NONE', #17406, 1000.000000000000000 ) ;
#17320=DIRECTION ( 'NONE',  ( 1.000000000000000000, 0.000000000000000000, -0.000000000000000000 ) ) ;
#17321=EDGE_CURVE ( 'NONE', #12399, #19270, #7002, .T. ) ;
#17325=EDGE_CURVE ( 'NONE', #3980, #8032, #3602, .T. ) ;
#17328=ORIENTED_EDGE ( 'NONE', *, *, #691, .T. ) ;
#17341=DIRECTION ( 'NONE',  ( 1.000000000000000000, 0.000000000000000000, 0.000000000000000000 ) ) ;
#17347=VERTEX_POINT ( 'NONE', #14511 ) ;
#17357=ORIENTED_EDGE ( 'NONE', *, *, #10134, .T. ) ;
#17358=( NAMED_UNIT ( * ) PLANE_ANGLE_UNIT ( ) SI_UNIT ( $, .RADIAN. ) );
#17371=ORIENTED_EDGE ( 'NONE', *, *, #13768, .F. ) ;
#17381=VECTOR ( 'NONE', #1065, 1000.000000000000000 ) ;
#17397=FILL_AREA_STYLE_COLOUR ( '', #8872 ) ;
#17398=ADVANCED_FACE ( 'NONE', ( #5545 ), #14927, .F. ) ;
#17399=ORIENTED_EDGE ( 'NONE', *, *, #4070, .F. ) ;
#17406=DIRECTION ( 'NONE',  ( 1.000000000000000000, -0.000000000000000000, -0.000000000000000000 ) ) ;
#17428=SURFACE_STYLE_FILL_AREA ( #7655 ) ;
#17431=ADVANCED_FACE ( 'NONE', ( #2138 ), #884, .T. ) ;
#17444=VERTEX_POINT ( 'NONE', #9140 ) ;
#17449=( LENGTH_UNIT ( ) NAMED_UNIT ( * ) SI_UNIT ( .MILLI., .METRE. ) );
#17451=DIRECTION ( 'NONE',  ( 0.000000000000000000, 0.000000000000000000, -1.000000000000000000 ) ) ;
#17460=AXIS2_PLACEMENT_3D ( 'NONE', #5271, #11546, #13602 ) ;
#17477=CYLINDRICAL_SURFACE ( 'NONE', #700, 10.00000000000001066 ) ;
#17484=DIRECTION ( 'NONE',  ( 0.000000000000000000, 0.000000000000000000, -1.000000000000000000 ) ) ;
#17489=DIRECTION ( 'NONE',  ( -0.000000000000000000, 0.000000000000000000, 1.000000000000000000 ) ) ;
#17490=DIRECTION ( 'NONE',  ( 1.000000000000000000, -0.000000000000000000, -0.000000000000000000 ) ) ;
#17496=DIRECTION ( 'NONE',  ( 0.000000000000000000, -1.000000000000000000, 0.000000000000000000 ) ) ;
#17500=FILL_AREA_STYLE_COLOUR ( '', #18787 ) ;
#17513=ORIENTED_EDGE ( 'NONE', *, *, #2069, .T. ) ;
#17515=CARTESIAN_POINT ( 'NONE',  ( 423.8334540492694487, 191.8198460455371333, 215.0057801310552179 ) ) ;
#17521=LINE ( 'NONE', #4969, #13010 ) ;
#17532=FACE_OUTER_BOUND ( 'NONE', #8348, .T. ) ;
#17567=FACE_OUTER_BOUND ( 'NONE', #20164, .T. ) ;
#17575=SURFACE_STYLE_FILL_AREA ( #9849 ) ;
#17578=CARTESIAN_POINT ( 'NONE',  ( 406.3334540492693350, 242.8734308960556234, 0.000000000000000000 ) ) ;
#17579=FILL_AREA_STYLE_COLOUR ( '', #5592 ) ;
#17583=COLOUR_RGB ( '', 0.09019608, 0.27058824, 0.51372549) ;
#17611=MECHANICAL_DESIGN_GEOMETRIC_PRESENTATION_REPRESENTATION('',(#14649),#10692);
#17626=CARTESIAN_POINT ( 'NONE',  ( 463.8334540492693350, 214.2156642432025251, 0.000000000000000000 ) ) ;
#17628=COLOUR_RGB ( '', 0.40784314, 0.44705882, 0.49803922) ;
#17639=ORIENTED_EDGE ( 'NONE', *, *, #13533, .T. ) ;
#17651=PRESENTATION_STYLE_ASSIGNMENT (( #11366 ) ) ;
#17663=ORIENTED_EDGE ( 'NONE', *, *, #11033, .T. ) ;
#17668=VERTEX_POINT ( 'NONE', #14895 ) ;
#17675=CARTESIAN_POINT ( 'NONE',  ( 463.8334540492693350, 191.8198460455371333, 14.99421986894475012 ) ) ;
#17677=DIRECTION ( 'NONE',  ( -0.000000000000000000, -0.000000000000000000, -1.000000000000000000 ) ) ;
#17696=DIRECTION ( 'NONE',  ( 1.000000000000000000, 1.197852309262419498E-15, -0.000000000000000000 ) ) ;
#17703=CARTESIAN_POINT ( 'NONE',  ( 498.8334540492693918, 167.8734308960555950, 0.000000000000000000 ) ) ;
#17709=( NAMED_UNIT ( * ) SI_UNIT ( $, .STERADIAN. ) SOLID_ANGLE_UNIT ( ) );
#17713=EDGE_CURVE ( 'NONE', #13911, #17228, #6974, .T. ) ;
#17716=ORIENTED_EDGE ( 'NONE', *, *, #843, .T. ) ;
#17719=AXIS2_PLACEMENT_3D ( 'NONE', #8594, #17777, #13373 ) ;
#17758=ORIENTED_EDGE ( 'NONE', *, *, #18804, .T. ) ;
#17764=FACE_BOUND ( 'NONE', #14018, .T. ) ;
#17777=DIRECTION ( 'NONE',  ( 1.000000000000000000, 0.000000000000000000, 0.000000000000000000 ) ) ;
#17791=( NAMED_UNIT ( * ) SI_UNIT ( $, .STERADIAN. ) SOLID_ANGLE_UNIT ( ) );
#17802=DIRECTION ( 'NONE',  ( 0.000000000000000000, 1.000000000000000000, 0.000000000000000000 ) ) ;
#17812=ORIENTED_EDGE ( 'NONE', *, *, #10679, .T. ) ;
#17814=( GEOMETRIC_REPRESENTATION_CONTEXT ( 3 ) GLOBAL_UNCERTAINTY_ASSIGNED_CONTEXT ( ( #2880 ) ) GLOBAL_UNIT_ASSIGNED_CONTEXT ( ( #3697, #2229, #17709 ) ) REPRESENTATION_CONTEXT ( 'NONE', 'WORKASPACE' ) );
#17816=ADVANCED_FACE ( 'NONE', ( #2523 ), #19616, .T. ) ;
#17826=EDGE_CURVE ( 'NONE', #6561, #14242, #11073, .T. ) ;
#17830=AXIS2_PLACEMENT_3D ( 'NONE', #12658, #8012, #12349 ) ;
#17851=DIRECTION ( 'NONE',  ( 0.000000000000000000, -1.000000000000000000, 0.000000000000000000 ) ) ;
#17865=ORIENTED_EDGE ( 'NONE', *, *, #5695, .F. ) ;
#17876=CARTESIAN_POINT ( 'NONE',  ( 458.8334540492693350, 242.8734308960556234, 0.000000000000000000 ) ) ;
#17877=( NAMED_UNIT ( * ) PLANE_ANGLE_UNIT ( ) SI_UNIT ( $, .RADIAN. ) );
#17885=VECTOR ( 'NONE', #4007, 1000.000000000000000 ) ;
#17887=( NAMED_UNIT ( * ) SI_UNIT ( $, .STERADIAN. ) SOLID_ANGLE_UNIT ( ) );
#17895=CIRCLE ( 'NONE', #13620, 10.00000000000000888 ) ;
#17898=CARTESIAN_POINT ( 'NONE',  ( 463.8334540492693350, 191.8198460455371333, 225.0057801310552463 ) ) ;
#17910=VECTOR ( 'NONE', #15241, 1000.000000000000000 ) ;
#17918=DIRECTION ( 'NONE',  ( 0.000000000000000000, 1.000000000000000000, 0.000000000000000000 ) ) ;
#17922=DIRECTION ( 'NONE',  ( 1.000000000000000000, 0.000000000000000000, -0.000000000000000000 ) ) ;
#17930=EDGE_CURVE ( 'NONE', #886, #12998, #4020, .T. ) ;
#17934=AXIS2_PLACEMENT_3D ( 'NONE', #15506, #3128, #1548 ) ;
#17964=EDGE_CURVE ( 'NONE', #17228, #5650, #19088, .T. ) ;
#17969=ORIENTED_EDGE ( 'NONE', *, *, #7588, .F. ) ;
#17979=CARTESIAN_POINT ( 'NONE',  ( 458.8334540492693350, 191.8198460455371333, 71.76606011801538898 ) ) ;
#18005=PRESENTATION_STYLE_ASSIGNMENT (( #13104 ) ) ;
#18027=DIRECTION ( 'NONE',  ( 0.000000000000000000, 0.000000000000000000, -1.000000000000000000 ) ) ;
#18036=EDGE_LOOP ( 'NONE', ( #977, #2393 ) ) ;
#18041=CARTESIAN_POINT ( 'NONE',  ( 463.8334540492693350, 214.2156642432025251, 0.000000000000000000 ) ) ;
#18049=EDGE_CURVE ( 'NONE', #6215, #11216, #6673, .T. ) ;
#18055=( GEOMETRIC_REPRESENTATION_CONTEXT ( 3 ) GLOBAL_UNCERTAINTY_ASSIGNED_CONTEXT ( ( #19698 ) ) GLOBAL_UNIT_ASSIGNED_CONTEXT ( ( #4693, #14171, #355 ) ) REPRESENTATION_CONTEXT ( 'NONE', 'WORKASPACE' ) );
#18069=DIRECTION ( 'NONE',  ( 1.000000000000000000, -0.000000000000000000, -0.000000000000000000 ) ) ;
#18070=EDGE_CURVE ( 'NONE', #10437, #8331, #7197, .T. ) ;
#18074=SURFACE_STYLE_USAGE ( .BOTH. , #12109 ) ;
#18080=VERTEX_POINT ( 'NONE', #15335 ) ;
#18083=EDGE_LOOP ( 'NONE', ( #9770, #7768 ) ) ;
#18085=SURFACE_STYLE_USAGE ( .BOTH. , #19250 ) ;
#18087=FILL_AREA_STYLE_COLOUR ( '', #9613 ) ;
#18092=CARTESIAN_POINT ( 'NONE',  ( 486.8117674897343363, 214.2156642432025251, 245.0000000000000000 ) ) ;
#18108=FACE_BOUND ( 'NONE', #11795, .T. ) ;
#18110=VECTOR ( 'NONE', #4884, 1000.000000000000000 ) ;
#18119=DIRECTION ( 'NONE',  ( 0.000000000000000000, 1.000000000000000000, 0.000000000000000000 ) ) ;
#18129=SURFACE_SIDE_STYLE ('',( #7233 ) ) ;
#18138=DIRECTION ( 'NONE',  ( 1.197852309262419498E-15, -1.000000000000000000, 0.000000000000000000 ) ) ;
#18148=AXIS2_PLACEMENT_3D ( 'NONE', #2842, #10683, #12219 ) ;
#18159=CIRCLE ( 'NONE', #12931, 10.00000000000000888 ) ;
#18162=PRESENTATION_STYLE_ASSIGNMENT (( #3665 ) ) ;
#18171=ADVANCED_FACE ( 'NONE', ( #10990 ), #54, .F. ) ;
#18180=EDGE_CURVE ( 'NONE', #15201, #20154, #10886, .T. ) ;
#18186=VECTOR ( 'NONE', #9282, 1000.000000000000000 ) ;
#18202=SURFACE_STYLE_FILL_AREA ( #10480 ) ;
#18208=CARTESIAN_POINT ( 'NONE',  ( 463.8334540492693350, 134.2156642432025251, 250.0000000000000000 ) ) ;
#18209=ORIENTED_EDGE ( 'NONE', *, *, #17930, .T. ) ;
#18210=EDGE_LOOP ( 'NONE', ( #3580, #10615, #16178, #16365, #5166, #13354, #12474, #5114, #7229, #7762, #14361, #8721 ) ) ;
#18211=VECTOR ( 'NONE', #5006, 1000.000000000000000 ) ;
#18225=DIRECTION ( 'NONE',  ( 1.000000000000000000, -0.000000000000000000, -0.000000000000000000 ) ) ;
#18229=( NAMED_UNIT ( * ) SI_UNIT ( $, .STERADIAN. ) SOLID_ANGLE_UNIT ( ) );
#18233=CIRCLE ( 'NONE', #9361, 10.00000000000000888 ) ;
#18237=CARTESIAN_POINT ( 'NONE',  ( 463.8334540492693350, 214.2156642432025251, 250.0000000000000000 ) ) ;
#18241=SURFACE_STYLE_FILL_AREA ( #8964 ) ;
#18263=VECTOR ( 'NONE', #11485, 1000.000000000000000 ) ;
#18267=ADVANCED_FACE ( 'NONE', ( #8422 ), #12963, .T. ) ;
#18276=AXIS2_PLACEMENT_3D ( 'NONE', #7978, #13969, #20248 ) ;
#18279=CARTESIAN_POINT ( 'NONE',  ( 463.8334540492693350, 134.2156642432025251, -87.31255586191144857 ) ) ;
#18289=ORIENTED_EDGE ( 'NONE', *, *, #7351, .F. ) ;
#18298=FILL_AREA_STYLE ('',( #5841 ) ) ;
#18323=FILL_AREA_STYLE_COLOUR ( '', #6060 ) ;
#18324=FILL_AREA_STYLE_COLOUR ( '', #4259 ) ;
#18334=EDGE_CURVE ( 'NONE', #664, #9734, #1312, .T. ) ;
#18335=ORIENTED_EDGE ( 'NONE', *, *, #5814, .T. ) ;
#18341=DIRECTION ( 'NONE',  ( 1.000000000000000000, 0.000000000000000000, 0.000000000000000000 ) ) ;
#18360=EDGE_LOOP ( 'NONE', ( #17120, #5225, #6981, #8438 ) ) ;
#18366=FILL_AREA_STYLE_COLOUR ( '', #17583 ) ;
#18367=CIRCLE ( 'NONE', #2895, 10.00000000000000888 ) ;
#18379=ORIENTED_EDGE ( 'NONE', *, *, #14435, .F. ) ;
#18381=MECHANICAL_DESIGN_GEOMETRIC_PRESENTATION_REPRESENTATION('',(#18725),#18055);
#18382=EDGE_LOOP ( 'NONE', ( #4601, #13958, #13131, #16995 ) ) ;
#18392=COLOUR_RGB ( '', 0.40784314, 0.44705882, 0.49803922) ;
#18409=VECTOR ( 'NONE', #11699, 1000.000000000000000 ) ;
#18415=( NAMED_UNIT ( * ) SI_UNIT ( $, .STERADIAN. ) SOLID_ANGLE_UNIT ( ) );
#18425=( LENGTH_UNIT ( ) NAMED_UNIT ( * ) SI_UNIT ( .MILLI., .METRE. ) );
#18429=EDGE_CURVE ( 'NONE', #8375, #5650, #5641, .T. ) ;
#18436=ORIENTED_EDGE ( 'NONE', *, *, #1797, .T. ) ;
#18443=CARTESIAN_POINT ( 'NONE',  ( 498.8117674897343932, 191.8198460455371333, 225.0057801310552463 ) ) ;
#18446=( NAMED_UNIT ( * ) PLANE_ANGLE_UNIT ( ) SI_UNIT ( $, .RADIAN. ) );
#18456=AXIS2_PLACEMENT_3D ( 'NONE', #18543, #1113, #15159 ) ;
#18460=DIRECTION ( 'NONE',  ( 1.000000000000000000, -0.000000000000000000, -0.000000000000000000 ) ) ;
#18479=ORIENTED_EDGE ( 'NONE', *, *, #1258, .F. ) ;
#18503=( NAMED_UNIT ( * ) PLANE_ANGLE_UNIT ( ) SI_UNIT ( $, .RADIAN. ) );
#18505=CARTESIAN_POINT ( 'NONE',  ( 498.8117674897343932, 191.8198460455371333, 34.99421986894476788 ) ) ;
#18506=ORIENTED_EDGE ( 'NONE', *, *, #10629, .T. ) ;
#18507=ORIENTED_EDGE ( 'NONE', *, *, #18070, .T. ) ;
#18508=STYLED_ITEM ( 'NONE', ( #17651 ), #13886 ) ;
#18510=COLOUR_RGB ( '', 0.66274510, 0.83137255, 0.94901961) ;
#18519=SURFACE_SIDE_STYLE ('',( #3063 ) ) ;
#18538=VECTOR ( 'NONE', #6992, 1000.000000000000000 ) ;
#18543=CARTESIAN_POINT ( 'NONE',  ( 458.8334540492693350, 191.8198460455371333, 168.2339398819845826 ) ) ;
#18545=DIRECTION ( 'NONE',  ( 0.000000000000000000, 0.000000000000000000, -1.000000000000000000 ) ) ;
#18550=CIRCLE ( 'NONE', #9353, 10.00000000000000888 ) ;
#18551=SURFACE_STYLE_FILL_AREA ( #19779 ) ;
#18556=PRESENTATION_STYLE_ASSIGNMENT (( #12279 ) ) ;
#18565=EDGE_LOOP ( 'NONE', ( #3240, #4199 ) ) ;
#18596=VECTOR ( 'NONE', #17851, 1000.000000000000000 ) ;
#18602=ORIENTED_EDGE ( 'NONE', *, *, #10266, .T. ) ;
#18605=ORIENTED_EDGE ( 'NONE', *, *, #14296, .F. ) ;
#18611=CARTESIAN_POINT ( 'NONE',  ( 498.8117674897343932, 134.2156642432025251, 250.0000000000000000 ) ) ;
#18614=EDGE_CURVE ( 'NONE', #17048, #16024, #2940, .T. ) ;
#18629=FILL_AREA_STYLE_COLOUR ( '', #20114 ) ;
#18634=SURFACE_STYLE_FILL_AREA ( #19750 ) ;
#18647=AXIS2_PLACEMENT_3D ( 'NONE', #7681, #10468, #4382 ) ;
#18656=( NAMED_UNIT ( * ) SI_UNIT ( $, .STERADIAN. ) SOLID_ANGLE_UNIT ( ) );
#18664=CARTESIAN_POINT ( 'NONE',  ( 458.8334540492693350, 0.000000000000000000, 250.0000000000000000 ) ) ;
#18669=APPLICATION_CONTEXT ( 'automotive_design' ) ;
#18679=CARTESIAN_POINT ( 'NONE',  ( 406.3334540492693350, 167.8734308960555950, 250.0000000000000000 ) ) ;
#18709=FILL_AREA_STYLE ('',( #6051 ) ) ;
#18711=CARTESIAN_POINT ( 'NONE',  ( 486.8117674897343363, 214.2156642432025251, 245.0000000000000000 ) ) ;
#18723=STYLED_ITEM ( 'NONE', ( #18556 ), #5118 ) ;
#18724=CARTESIAN_POINT ( 'NONE',  ( 498.8117674897343932, 191.8198460455371333, 91.76606011801541740 ) ) ;
#18725=STYLED_ITEM ( 'NONE', ( #12849 ), #10935 ) ;
#18744=ORIENTED_EDGE ( 'NONE', *, *, #16352, .T. ) ;
#18745=( LENGTH_UNIT ( ) NAMED_UNIT ( * ) SI_UNIT ( .MILLI., .METRE. ) );
#18748=MECHANICAL_DESIGN_GEOMETRIC_PRESENTATION_REPRESENTATION('',(#15482),#19719);
#18749=CYLINDRICAL_SURFACE ( 'NONE', #16354, 10.00000000000001066 ) ;
#18758=SURFACE_STYLE_USAGE ( .BOTH. , #18965 ) ;
#18787=COLOUR_RGB ( '', 0.31764706, 0.68627451, 0.89019608) ;
#18791=( LENGTH_UNIT ( ) NAMED_UNIT ( * ) SI_UNIT ( .MILLI., .METRE. ) );
#18800=SURFACE_SIDE_STYLE ('',( #12333 ) ) ;
#18803=CARTESIAN_POINT ( 'NONE',  ( 463.8334540492693350, 191.8198460455371333, 178.2339398819846110 ) ) ;
#18804=EDGE_CURVE ( 'NONE', #6007, #16512, #6361, .T. ) ;
#18811=FILL_AREA_STYLE_COLOUR ( '', #15871 ) ;
#18832=( GEOMETRIC_REPRESENTATION_CONTEXT ( 3 ) GLOBAL_UNCERTAINTY_ASSIGNED_CONTEXT ( ( #6493 ) ) GLOBAL_UNIT_ASSIGNED_CONTEXT ( ( #19627, #20341, #18994 ) ) REPRESENTATION_CONTEXT ( 'NONE', 'WORKASPACE' ) );
#18833=ADVANCED_FACE ( 'NONE', ( #11598 ), #14892, .F. ) ;
#18835=ORIENTED_EDGE ( 'NONE', *, *, #4825, .T. ) ;
#18840=ORIENTED_EDGE ( 'NONE', *, *, #10, .T. ) ;
#18871=STYLED_ITEM ( 'NONE', ( #4575 ), #19037 ) ;
#18876=VECTOR ( 'NONE', #15388, 1000.000000000000000 ) ;
#18880=DIRECTION ( 'NONE',  ( -1.000000000000000000, 0.000000000000000000, 0.000000000000000000 ) ) ;
#18884=EDGE_LOOP ( 'NONE', ( #2804, #17098, #7281, #11527 ) ) ;
#18885=VECTOR ( 'NONE', #19353, 1000.000000000000000 ) ;
#18892=VECTOR ( 'NONE', #9332, 1000.000000000000000 ) ;
#18901=SURFACE_SIDE_STYLE ('',( #6248 ) ) ;
#18912=CIRCLE ( 'NONE', #10044, 10.00000000000000888 ) ;
#18924=SURFACE_SIDE_STYLE ('',( #9547 ) ) ;
#18936=AXIS2_PLACEMENT_3D ( 'NONE', #3556, #14769, #4152 ) ;
#18946=EDGE_CURVE ( 'NONE', #13149, #16512, #15195, .T. ) ;
#18961=LINE ( 'NONE', #1626, #1529 ) ;
#18965=SURFACE_SIDE_STYLE ('',( #14041 ) ) ;
#18994=( NAMED_UNIT ( * ) SI_UNIT ( $, .STERADIAN. ) SOLID_ANGLE_UNIT ( ) );
#19017=ORIENTED_EDGE ( 'NONE', *, *, #15437, .F. ) ;
#19021=CARTESIAN_POINT ( 'NONE',  ( 423.8334540492694487, 191.8198460455371333, 235.0057801310552463 ) ) ;
#19037=ADVANCED_FACE ( 'NONE', ( #10653 ), #15408, .F. ) ;
#19041=SURFACE_SIDE_STYLE ('',( #9686 ) ) ;
#19046=DIRECTION ( 'NONE',  ( 1.000000000000000000, 0.000000000000000000, 0.000000000000000000 ) ) ;
#19056=DIRECTION ( 'NONE',  ( 1.000000000000000000, 0.000000000000000000, -0.000000000000000000 ) ) ;
#19082=CARTESIAN_POINT ( 'NONE',  ( 493.8117674897343363, 134.2156642432025251, 245.0000000000000000 ) ) ;
#19088=LINE ( 'NONE', #3652, #12234 ) ;
#19113=DIRECTION ( 'NONE',  ( 0.000000000000000000, -1.000000000000000000, 0.000000000000000000 ) ) ;
#19120=VECTOR ( 'NONE', #3807, 1000.000000000000000 ) ;
#19121=( GEOMETRIC_REPRESENTATION_CONTEXT ( 3 ) GLOBAL_UNCERTAINTY_ASSIGNED_CONTEXT ( ( #11995 ) ) GLOBAL_UNIT_ASSIGNED_CONTEXT ( ( #6608, #14028, #9387 ) ) REPRESENTATION_CONTEXT ( 'NONE', 'WORKASPACE' ) );
#19137=CARTESIAN_POINT ( 'NONE',  ( 503.8334540492693918, 191.8198460455371333, 81.76606011801540319 ) ) ;
#19150=ORIENTED_EDGE ( 'NONE', *, *, #9406, .T. ) ;
#19153=( GEOMETRIC_REPRESENTATION_CONTEXT ( 3 ) GLOBAL_UNCERTAINTY_ASSIGNED_CONTEXT ( ( #5549 ) ) GLOBAL_UNIT_ASSIGNED_CONTEXT ( ( #5019, #7696, #14178 ) ) REPRESENTATION_CONTEXT ( 'NONE', 'WORKASPACE' ) );
#19155=FILL_AREA_STYLE_COLOUR ( '', #9863 ) ;
#19162=AXIS2_PLACEMENT_3D ( 'NONE', #16369, #3361, #2104 ) ;
#19164=CYLINDRICAL_SURFACE ( 'NONE', #17460, 10.00000000000001066 ) ;
#19167=( NAMED_UNIT ( * ) SI_UNIT ( $, .STERADIAN. ) SOLID_ANGLE_UNIT ( ) );
#19190=SURFACE_STYLE_USAGE ( .BOTH. , #12928 ) ;
#19193=VERTEX_POINT ( 'NONE', #2183 ) ;
#19222=DIRECTION ( 'NONE',  ( 0.000000000000000000, 0.000000000000000000, 1.000000000000000000 ) ) ;
#19224=CARTESIAN_POINT ( 'NONE',  ( 423.8334540492694487, 191.8198460455371333, 168.2339398819845826 ) ) ;
#19231=DIRECTION ( 'NONE',  ( 0.000000000000000000, 0.000000000000000000, -1.000000000000000000 ) ) ;
#19237=FACE_OUTER_BOUND ( 'NONE', #10183, .T. ) ;
#19240=( GEOMETRIC_REPRESENTATION_CONTEXT ( 3 ) GLOBAL_UNCERTAINTY_ASSIGNED_CONTEXT ( ( #4337 ) ) GLOBAL_UNIT_ASSIGNED_CONTEXT ( ( #19870, #2359, #7317 ) ) REPRESENTATION_CONTEXT ( 'NONE', 'WORKASPACE' ) );
#19246=( LENGTH_UNIT ( ) NAMED_UNIT ( * ) SI_UNIT ( .MILLI., .METRE. ) );
#19247=CARTESIAN_POINT ( 'NONE',  ( 475.8334540492694487, 214.2156642432025251, 250.0000000000000000 ) ) ;
#19250=SURFACE_SIDE_STYLE ('',( #13092 ) ) ;
#19253=ORIENTED_EDGE ( 'NONE', *, *, #17325, .F. ) ;
#19267=VECTOR ( 'NONE', #2960, 1000.000000000000000 ) ;
#19270=VERTEX_POINT ( 'NONE', #15175 ) ;
#19276=FACE_BOUND ( 'NONE', #273, .T. ) ;
#19311=CARTESIAN_POINT ( 'NONE',  ( 493.8117674897343363, 214.2156642432025251, 245.0000000000000000 ) ) ;
#19315=EDGE_CURVE ( 'NONE', #7492, #8848, #13967, .T. ) ;
#19330=PRESENTATION_STYLE_ASSIGNMENT (( #8125 ) ) ;
#19349=ORIENTED_EDGE ( 'NONE', *, *, #14530, .F. ) ;
#19352=CARTESIAN_POINT ( 'NONE',  ( 423.8334540492694487, 191.8198460455371333, 178.2339398819846110 ) ) ;
#19353=DIRECTION ( 'NONE',  ( -0.000000000000000000, -0.000000000000000000, 1.000000000000000000 ) ) ;
#19356=LINE ( 'NONE', #1931, #1749 ) ;
#19370=UNCERTAINTY_MEASURE_WITH_UNIT (LENGTH_MEASURE( 1.000000000000000082E-05 ), #1095, 'distance_accuracy_value', 'NONE');
#19381=MECHANICAL_DESIGN_GEOMETRIC_PRESENTATION_REPRESENTATION('',(#15132),#12158);
#19388=CARTESIAN_POINT ( 'NONE',  ( 463.8334540492693350, 191.8198460455371333, 14.99421986894475012 ) ) ;
#19402=DIRECTION ( 'NONE',  ( -0.000000000000000000, 1.000000000000000000, -0.000000000000000000 ) ) ;
#19403=ORIENTED_EDGE ( 'NONE', *, *, #3831, .T. ) ;
#19404=CARTESIAN_POINT ( 'NONE',  ( 463.8334540492693350, 214.2156642432025251, 250.0000000000000000 ) ) ;
#19420=AXIS2_PLACEMENT_3D ( 'NONE', #2795, #4347, #7050 ) ;
#19430=SURFACE_SIDE_STYLE ('',( #13184 ) ) ;
#19435=EDGE_CURVE ( 'NONE', #951, #5981, #11452, .T. ) ;
#19437=DIRECTION ( 'NONE',  ( 1.000000000000000000, 1.197852309262419498E-15, -0.000000000000000000 ) ) ;
#19440=DIRECTION ( 'NONE',  ( 1.000000000000000000, -0.000000000000000000, -0.000000000000000000 ) ) ;
#19460=FILL_AREA_STYLE ('',( #6931 ) ) ;
#19467=ORIENTED_EDGE ( 'NONE', *, *, #8091, .F. ) ;
#19471=DIRECTION ( 'NONE',  ( 0.000000000000000000, 0.000000000000000000, -1.000000000000000000 ) ) ;
#19479=DIRECTION ( 'NONE',  ( 1.000000000000000000, -0.000000000000000000, -0.000000000000000000 ) ) ;
#19481=VECTOR ( 'NONE', #4760, 1000.000000000000000 ) ;
#19488=VECTOR ( 'NONE', #10386, 1000.000000000000000 ) ;
#19495=LINE ( 'NONE', #5411, #18409 ) ;
#19497=DIRECTION ( 'NONE',  ( 0.000000000000000000, 0.000000000000000000, -1.000000000000000000 ) ) ;
#19499=VECTOR ( 'NONE', #4248, 1000.000000000000000 ) ;
#19505=( LENGTH_UNIT ( ) NAMED_UNIT ( * ) SI_UNIT ( .MILLI., .METRE. ) );
#19523=MECHANICAL_DESIGN_GEOMETRIC_PRESENTATION_REPRESENTATION('',(#1407),#13315);
#19568=DIRECTION ( 'NONE',  ( 1.000000000000000000, 0.000000000000000000, 0.000000000000000000 ) ) ;
#19580=CARTESIAN_POINT ( 'NONE',  ( 498.8334540492693918, 191.8198460455371333, 14.99421986894475012 ) ) ;
#19583=ADVANCED_FACE ( 'NONE', ( #611 ), #3829, .F. ) ;
#19616=PLANE ( 'NONE',  #16535 ) ;
#19618=VECTOR ( 'NONE', #13269, 1000.000000000000000 ) ;
#19627=( LENGTH_UNIT ( ) NAMED_UNIT ( * ) SI_UNIT ( .MILLI., .METRE. ) );
#19630=PLANE ( 'NONE',  #14790 ) ;
#19633=CARTESIAN_POINT ( 'NONE',  ( 498.8334540492693918, 214.2156642432025251, 250.0000000000000000 ) ) ;
#19634=DIRECTION ( 'NONE',  ( 0.000000000000000000, 1.000000000000000000, -0.000000000000000000 ) ) ;
#19648=SURFACE_STYLE_FILL_AREA ( #14944 ) ;
#19651=EDGE_CURVE ( 'NONE', #12704, #8671, #18233, .T. ) ;
#19656=PRESENTATION_STYLE_ASSIGNMENT (( #1096 ) ) ;
#19659=SURFACE_STYLE_USAGE ( .BOTH. , #10109 ) ;
#19664=FACE_BOUND ( 'NONE', #18036, .T. ) ;
#19665=ORIENTED_EDGE ( 'NONE', *, *, #5902, .F. ) ;
#19668=DIRECTION ( 'NONE',  ( -1.000000000000000000, 0.000000000000000000, -0.000000000000000000 ) ) ;
#19687=AXIS2_PLACEMENT_3D ( 'NONE', #4645, #9173, #98 ) ;
#19689=EDGE_LOOP ( 'NONE', ( #11514, #13855, #5926, #8667 ) ) ;
#19698=UNCERTAINTY_MEASURE_WITH_UNIT (LENGTH_MEASURE( 1.000000000000000082E-05 ), #4693, 'distance_accuracy_value', 'NONE');
#19706=MECHANICAL_DESIGN_GEOMETRIC_PRESENTATION_REPRESENTATION('',(#12833),#2263);
#19711=ORIENTED_EDGE ( 'NONE', *, *, #1737, .T. ) ;
#19719=( GEOMETRIC_REPRESENTATION_CONTEXT ( 3 ) GLOBAL_UNCERTAINTY_ASSIGNED_CONTEXT ( ( #5380 ) ) GLOBAL_UNIT_ASSIGNED_CONTEXT ( ( #266, #14390, #12860 ) ) REPRESENTATION_CONTEXT ( 'NONE', 'WORKASPACE' ) );
#19722=PLANE ( 'NONE',  #3135 ) ;
#19723=COLOUR_RGB ( '', 0.08235294, 0.09019608, 0.10196078) ;
#19745=MECHANICAL_DESIGN_GEOMETRIC_PRESENTATION_REPRESENTATION('',(#17123),#7278);
#19746=ORIENTED_EDGE ( 'NONE', *, *, #10629, .F. ) ;
#19750=FILL_AREA_STYLE ('',( #18323 ) ) ;
#19751=DIRECTION ( 'NONE',  ( -1.000000000000000000, -0.000000000000000000, -0.000000000000000000 ) ) ;
#19754=VECTOR ( 'NONE', #4972, 1000.000000000000000 ) ;
#19761=( NAMED_UNIT ( * ) PLANE_ANGLE_UNIT ( ) SI_UNIT ( $, .RADIAN. ) );
#19770=UNCERTAINTY_MEASURE_WITH_UNIT (LENGTH_MEASURE( 1.000000000000000082E-05 ), #19505, 'distance_accuracy_value', 'NONE');
#19779=FILL_AREA_STYLE ('',( #5582 ) ) ;
#19783=STYLED_ITEM ( 'NONE', ( #10798 ), #8611 ) ;
#19795=UNCERTAINTY_MEASURE_WITH_UNIT (LENGTH_MEASURE( 1.000000000000000082E-05 ), #15422, 'distance_accuracy_value', 'NONE');
#19814=ORIENTED_EDGE ( 'NONE', *, *, #3344, .T. ) ;
#19820=CARTESIAN_POINT ( 'NONE',  ( 498.8334540492693918, 191.8198460455371333, 34.99421986894476788 ) ) ;
#19838=FILL_AREA_STYLE_COLOUR ( '', #13988 ) ;
#19845=DIRECTION ( 'NONE',  ( 1.000000000000000000, 0.000000000000000000, 0.000000000000000000 ) ) ;
#19849=COLOUR_RGB ( '', 0.72549020, 0.75294118, 0.79215686) ;
#19856=ADVANCED_FACE ( 'NONE', ( #434 ), #6947, .F. ) ;
#19870=( LENGTH_UNIT ( ) NAMED_UNIT ( * ) SI_UNIT ( .MILLI., .METRE. ) );
#19880=PRESENTATION_STYLE_ASSIGNMENT (( #7537 ) ) ;
#19890=CYLINDRICAL_SURFACE ( 'NONE', #15297, 10.00000000000000888 ) ;
#19893=AXIS2_PLACEMENT_3D ( 'NONE', #14947, #7495, #16979 ) ;
#19914=ORIENTED_EDGE ( 'NONE', *, *, #9990, .T. ) ;
#19922=ORIENTED_EDGE ( 'NONE', *, *, #3563, .F. ) ;
#19945=LINE ( 'NONE', #10393, #7885 ) ;
#19947=EDGE_CURVE ( 'NONE', #13170, #6967, #8574, .T. ) ;
#19970=ORIENTED_EDGE ( 'NONE', *, *, #4733, .T. ) ;
#19978=VECTOR ( 'NONE', #10852, 1000.000000000000000 ) ;
#19981=FILL_AREA_STYLE_COLOUR ( '', #11302 ) ;
#19986=DIRECTION ( 'NONE',  ( 0.000000000000000000, 0.000000000000000000, -1.000000000000000000 ) ) ;
#19992=EDGE_LOOP ( 'NONE', ( #12200, #3397, #12939, #8995 ) ) ;
#19997=EDGE_LOOP ( 'NONE', ( #19711, #10587, #9980, #9012 ) ) ;
#20004=DIRECTION ( 'NONE',  ( 1.000000000000000000, -0.000000000000000000, -0.000000000000000000 ) ) ;
#20016=MECHANICAL_DESIGN_GEOMETRIC_PRESENTATION_REPRESENTATION('',(#18723),#14770);
#20022=SURFACE_STYLE_FILL_AREA ( #18298 ) ;
#20023=SURFACE_STYLE_FILL_AREA ( #13675 ) ;
#20027=CARTESIAN_POINT ( 'NONE',  ( 458.8334540492693350, 191.8198460455371333, 168.2339398819845826 ) ) ;
#20038=SURFACE_SIDE_STYLE ('',( #7199 ) ) ;
#20043=AXIS2_PLACEMENT_3D ( 'NONE', #6676, #1897, #3576 ) ;
#20062=AXIS2_PLACEMENT_3D ( 'NONE', #10302, #7433, #8768 ) ;
#20082=AXIS2_PLACEMENT_3D ( 'NONE', #9672, #17490, #10921 ) ;
#20097=FACE_OUTER_BOUND ( 'NONE', #2164, .T. ) ;
#20101=COLOUR_RGB ( '', 0.09019608, 0.27058824, 0.51372549) ;
#20114=COLOUR_RGB ( '', 0.09019608, 0.27058824, 0.51372549) ;
#20123=DIRECTION ( 'NONE',  ( 1.000000000000000000, 0.000000000000000000, 0.000000000000000000 ) ) ;
#20126=EDGE_LOOP ( 'NONE', ( #15008, #544, #11848, #11869 ) ) ;
#20135=MECHANICAL_DESIGN_GEOMETRIC_PRESENTATION_REPRESENTATION('',(#11942),#12593);
#20145=LINE ( 'NONE', #18711, #13036 ) ;
#20149=( LENGTH_UNIT ( ) NAMED_UNIT ( * ) SI_UNIT ( .MILLI., .METRE. ) );
#20154=VERTEX_POINT ( 'NONE', #7721 ) ;
#20164=EDGE_LOOP ( 'NONE', ( #5915, #19150, #19914, #15825 ) ) ;
#20165=DIRECTION ( 'NONE',  ( -0.000000000000000000, 0.000000000000000000, 1.000000000000000000 ) ) ;
#20175=SURFACE_STYLE_FILL_AREA ( #12251 ) ;
#20176=SURFACE_STYLE_USAGE ( .BOTH. , #2564 ) ;
#20184=ORIENTED_EDGE ( 'NONE', *, *, #1390, .F. ) ;
#20198=CIRCLE ( 'NONE', #1083, 10.00000000000000888 ) ;
#20208=MECHANICAL_DESIGN_GEOMETRIC_PRESENTATION_REPRESENTATION('',(#8702),#6752);
#20217=VECTOR ( 'NONE', #3440, 1000.000000000000000 ) ;
#20227=VECTOR ( 'NONE', #10397, 1000.000000000000000 ) ;
#20236=CIRCLE ( 'NONE', #16649, 10.00000000000000888 ) ;
#20248=DIRECTION ( 'NONE',  ( 0.000000000000000000, 0.000000000000000000, -1.000000000000000000 ) ) ;
#20260=DIRECTION ( 'NONE',  ( 1.000000000000000000, -0.000000000000000000, -0.000000000000000000 ) ) ;
#20275=AXIS2_PLACEMENT_3D ( 'NONE', #16011, #1842, #8248 ) ;
#20278=FILL_AREA_STYLE_COLOUR ( '', #110 ) ;
#20289=ORIENTED_EDGE ( 'NONE', *, *, #672, .T. ) ;
#20293=PLANE ( 'NONE',  #9333 ) ;
#20297=DIRECTION ( 'NONE',  ( 1.000000000000000000, 0.000000000000000000, -0.000000000000000000 ) ) ;
#20302=DIRECTION ( 'NONE',  ( 1.000000000000000000, -0.000000000000000000, -0.000000000000000000 ) ) ;
#20315=( LENGTH_UNIT ( ) NAMED_UNIT ( * ) SI_UNIT ( .MILLI., .METRE. ) );
#20340=PRESENTATION_STYLE_ASSIGNMENT (( #1673 ) ) ;
#20341=( NAMED_UNIT ( * ) PLANE_ANGLE_UNIT ( ) SI_UNIT ( $, .RADIAN. ) );
#20357=ORIENTED_EDGE ( 'NONE', *, *, #10266, .F. ) ;
#20367=VERTEX_POINT ( 'NONE', #14505 ) ;
#20368=FACE_OUTER_BOUND ( 'NONE', #17308, .T. ) ;
ENDSEC;
END-ISO-10303-21;
